ISO-10303-21;
HEADER;
FILE_DESCRIPTION (('STEP AP214'),
    '1' );
FILE_NAME ('Handle Screw.step',
    '2026-10-06T09:49:54',
    ( '' ),
    ( '' ),
    'SwSTEP 2.0',
    'SolidWorks 2020',
    '' );
FILE_SCHEMA (( 'AUTOMOTIVE_DESIGN' ));
ENDSEC;

DATA;
#50=CARTESIAN_POINT ( 'NONE',  ( -8.821555121468717786, 1364.295427727885453, 207.6218459616988241 ) ) ;
#59=CARTESIAN_POINT ( 'NONE',  ( -7.009540617219531811, 1370.193319312941412, 208.3718459617010978 ) ) ;
#78=TOROIDAL_SURFACE ( 'NONE', #103817, 9.500000000000000000, 0.5000000000000000000 ) ;
#342=CARTESIAN_POINT ( 'NONE',  ( 9.369782510130001185, 1366.497526915280105, 207.6218459616989946 ) ) ;
#356=CARTESIAN_POINT ( 'NONE',  ( 4.911313360425503483, 1370.788543751794350, 208.3718459617010978 ) ) ;
#372=EDGE_CURVE ( 'NONE', #74254, #52548, #25231, .T. ) ;
#430=CARTESIAN_POINT ( 'NONE',  ( -9.724834716106559089E-16, 1374.031200045389824, 209.1218459616989946 ) ) ;
#437=VERTEX_POINT ( 'NONE', #42792 ) ;
#488=CARTESIAN_POINT ( 'NONE',  ( 1.748848150595841977, 1360.440694539930064, 210.6218459616991936 ) ) ;
#513=CARTESIAN_POINT ( 'NONE',  ( -2.724500461543110319, 1367.224846223802842, 209.6218459617148824 ) ) ;
#602=CARTESIAN_POINT ( 'NONE',  ( -7.406989585696536871, 1364.221058288796257, 209.6218459617148824 ) ) ;
#610=CARTESIAN_POINT ( 'NONE',  ( -10.65892733151780369, 1368.068496973798574, 209.6218459617033432 ) ) ;
#617=ORIENTED_EDGE ( 'NONE', *, *, #44729, .F. ) ;
#807=ADVANCED_FACE ( 'NONE', ( #11949 ), #61288, .F. ) ;
#889=CARTESIAN_POINT ( 'NONE',  ( 8.788288708663037241, 1364.745218052601786, 210.6218459617142003 ) ) ;
#901=CARTESIAN_POINT ( 'NONE',  ( 8.279480055211028144, 1369.617909351883327, 208.3718459617010978 ) ) ;
#913=CARTESIAN_POINT ( 'NONE',  ( -9.832966357650001044, 1364.062280235949856, 207.6218459616989946 ) ) ;
#919=ORIENTED_EDGE ( 'NONE', *, *, #372, .T. ) ;
#1039=CARTESIAN_POINT ( 'NONE',  ( -0.7957830110718832062, 1359.403009717480018, 207.6218459616987673 ) ) ;
#1062=CARTESIAN_POINT ( 'NONE',  ( -4.743735107867810719, 1366.962391455512034, 208.3718459617061285 ) ) ;
#1139=CARTESIAN_POINT ( 'NONE',  ( -2.831065174598700551, 1367.763066558967012, 208.7333235891643142 ) ) ;
#1156=CARTESIAN_POINT ( 'NONE',  ( -6.674371810360079316, 1362.851205800406888, 210.6218459617142003 ) ) ;
#1160=DIRECTION ( 'NONE',  ( 0.000000000000000000, -2.700129756073415263E-15, -1.000000000000000000 ) ) ;
#1164=CARTESIAN_POINT ( 'NONE',  ( -7.811405798887459895, 1367.739269854435861, 210.6218459616991936 ) ) ;
#1227=VERTEX_POINT ( 'NONE', #62367 ) ;
#1397=AXIS2_PLACEMENT_3D ( 'NONE', #83042, #57321, #98183 ) ;
#1422=CARTESIAN_POINT ( 'NONE',  ( 8.829530141155370160, 1365.516248932926601, 207.6218459616988241 ) ) ;
#1435=CARTESIAN_POINT ( 'NONE',  ( 8.305289958184035370, 1368.611760151032058, 207.6218459616987673 ) ) ;
#1446=CARTESIAN_POINT ( 'NONE',  ( -4.533972342531168209, 1368.949167379208347, 207.6218459616989946 ) ) ;
#1549=ORIENTED_EDGE ( 'NONE', *, *, #45523, .F. ) ;
#1582=CARTESIAN_POINT ( 'NONE',  ( 3.726002059892866480, 1358.803007711198916, 208.3718459617010978 ) ) ;
#1609=CARTESIAN_POINT ( 'NONE',  ( -7.811405798920000088, 1367.739269854440181, 207.6218459616989946 ) ) ;
#1690=CARTESIAN_POINT ( 'NONE',  ( -2.852161174780241559, 1367.911847845928150, 208.3703648968576942 ) ) ;
#1700=AXIS2_PLACEMENT_3D ( 'NONE', #47499, #79993, #57014 ) ;
#1708=CARTESIAN_POINT ( 'NONE',  ( -7.910792383497443403, 1364.512313338026843, 208.3718459617061285 ) ) ;
#1718=CARTESIAN_POINT ( 'NONE',  ( -9.441793314685410721, 1368.076698943698375, 210.6218459617030021 ) ) ;
#1730=ORIENTED_EDGE ( 'NONE', *, *, #66449, .F. ) ;
#1803=CARTESIAN_POINT ( 'NONE',  ( 4.225988784556967914, 1370.419465002912375, 209.6763548415352432 ) ) ;
#1843=CARTESIAN_POINT ( 'NONE',  ( -1.105745987349477488, 1370.041125217912850, 206.9838924340121196 ) ) ;
#1863=CARTESIAN_POINT ( 'NONE',  ( -8.696701630030000629, 1367.135748871429996, 210.6218459616991936 ) ) ;
#1997=CARTESIAN_POINT ( 'NONE',  ( 9.671060821790000261, 1366.060403940050037, 207.6218459616989946 ) ) ;
#2022=CARTESIAN_POINT ( 'NONE',  ( 8.379275254590000443, 1362.454991452509830, 207.6218459616989946 ) ) ;
#2150=CARTESIAN_POINT ( 'NONE',  ( 9.444074105595053226, 1360.911098639617876, 208.3718459617010978 ) ) ;
#2177=CARTESIAN_POINT ( 'NONE',  ( -5.236338392966255917, 1368.774323667083991, 210.6218459616987957 ) ) ;
#2192=ORIENTED_EDGE ( 'NONE', *, *, #46877, .T. ) ;
#2258=CARTESIAN_POINT ( 'NONE',  ( -2.928726385117801367, 1368.451830327553807, 207.8117072160285090 ) ) ;
#2274=CARTESIAN_POINT ( 'NONE',  ( -5.675785208868349585, 1362.218944691939669, 207.6218459616988241 ) ) ;
#2282=CARTESIAN_POINT ( 'NONE',  ( -8.284884219063519240, 1369.613879705106001, 208.3718459617010978 ) ) ;
#2320=( LENGTH_UNIT ( ) NAMED_UNIT ( * ) SI_UNIT ( .MILLI., .METRE. ) );
#2423=CARTESIAN_POINT ( 'NONE',  ( -9.655745333040000489, 1363.739547551589794, 210.6218459616991936 ) ) ;
#2555=CARTESIAN_POINT ( 'NONE',  ( 8.553883624160958377, 1365.586653183476074, 210.6218459617142003 ) ) ;
#2580=CARTESIAN_POINT ( 'NONE',  ( 10.02176186330000007, 1364.879735892739973, 207.6218459616989946 ) ) ;
#2700=CARTESIAN_POINT ( 'NONE',  ( 10.24616803579280955, 1362.814633186277206, 207.6218459616987673 ) ) ;
#2725=CARTESIAN_POINT ( 'NONE',  ( -7.454882155592339465, 1365.567498750975801, 209.6218459617148824 ) ) ;
#2822=CARTESIAN_POINT ( 'NONE',  ( -9.690020260104200034, 1366.026910387847920, 210.6218459616991936 ) ) ;
#3019=EDGE_CURVE ( 'NONE', #74254, #18150, #87284, .T. ) ;
#3067=DIRECTION ( 'NONE',  ( 0.8775825618903732028, -4.965288137873349002E-32, 0.4794255386042021172 ) ) ;
#3104=CARTESIAN_POINT ( 'NONE',  ( 7.818221670759999853, 1367.736483592530021, 207.6218459616989946 ) ) ;
#3130=CARTESIAN_POINT ( 'NONE',  ( -2.380813228419999650, 1360.502616939890004, 207.6218459616989946 ) ) ;
#3131=CIRCLE ( 'NONE', #24488, 0.4999999999999980016 ) ;
#3253=CARTESIAN_POINT ( 'NONE',  ( 7.877099145829999038, 1362.118768394180051, 207.6218459616989946 ) ) ;
#3275=CARTESIAN_POINT ( 'NONE',  ( -4.710894888870413411, 1366.841595974748316, 209.6218459617148824 ) ) ;
#3293=VERTEX_POINT ( 'NONE', #73824 ) ;
#3374=CARTESIAN_POINT ( 'NONE',  ( -11.37387391107785994, 1367.111335829282325, 209.6218459617033432 ) ) ;
#3377=CIRCLE ( 'NONE', #67716, 10.00000000000000888 ) ;
#3481=CARTESIAN_POINT ( 'NONE',  ( 0.9603421195823178547, 1368.656381476072966, 207.8228078564805230 ) ) ;
#3518=CARTESIAN_POINT ( 'NONE',  ( -9.830395177430000686, 1365.769828494180047, 210.6218459616991936 ) ) ;
#3590=CARTESIAN_POINT ( 'NONE',  ( -3.071538966616310429, 1374.913060387290216, 207.4438565765843236 ) ) ;
#3656=CARTESIAN_POINT ( 'NONE',  ( 7.706598004008788472, 1366.632089620137322, 207.6218459616988241 ) ) ;
#3684=EDGE_CURVE ( 'NONE', #18150, #15971, #12215, .T. ) ;
#3807=CARTESIAN_POINT ( 'NONE',  ( 6.892224678230459034, 1361.632554499760090, 210.6218459616991936 ) ) ;
#3831=CARTESIAN_POINT ( 'NONE',  ( -9.657355732020000971, 1366.083296228050131, 207.6218459616989946 ) ) ;
#3925=CARTESIAN_POINT ( 'NONE',  ( -10.68726663944961963, 1366.700119988787719, 210.6218459617030021 ) ) ;
#4024=DIRECTION ( 'NONE',  ( -0.8775825618903722036, 0.000000000000000000, -0.4794255386042038936 ) ) ;
#4062=CARTESIAN_POINT ( 'NONE',  ( 0.05823133897709759782, 1360.390585217549869, 210.6218459616991936 ) ) ;
#4183=CARTESIAN_POINT ( 'NONE',  ( 9.231361398829999843, 1366.659448741839924, 207.6218459616989946 ) ) ;
#4197=DIRECTION ( 'NONE',  ( 0.8775825618903727587, 9.629649721936177897E-33, 0.4794255386042027833 ) ) ;
#4208=EDGE_CURVE ( 'NONE', #40999, #32037, #63879, .T. ) ;
#4321=CARTESIAN_POINT ( 'NONE',  ( 3.107265622092247881, 1362.633694524574594, 209.6218459617148824 ) ) ;
#4338=CARTESIAN_POINT ( 'NONE',  ( 9.790769103959343411, 1362.302375259238488, 207.6218459616987673 ) ) ;
#4363=CARTESIAN_POINT ( 'NONE',  ( -8.968861126993214583, 1364.620492801554747, 207.6218459616988241 ) ) ;
#4461=CARTESIAN_POINT ( 'NONE',  ( -10.78183993585174427, 1367.738238001941909, 208.3718459617010978 ) ) ;
#4515=DIRECTION ( 'NONE',  ( 3.828568698926946970E-16, 0.000000000000000000, -1.000000000000000000 ) ) ;
#4578=ORIENTED_EDGE ( 'NONE', *, *, #83626, .T. ) ;
#4597=CARTESIAN_POINT ( 'NONE',  ( 8.653423937779999520, 1367.169888897630017, 210.6218459616991936 ) ) ;
#4718=CARTESIAN_POINT ( 'NONE',  ( 8.726849315049442168, 1367.111769039830051, 210.6218459616987957 ) ) ;
#4743=CARTESIAN_POINT ( 'NONE',  ( 8.988338641399998608, 1366.896325247149889, 207.6218459616989946 ) ) ;
#4847=CARTESIAN_POINT ( 'NONE',  ( -2.252062897235808769, 1361.698003988630035, 210.6218459617142003 ) ) ;
#4866=CARTESIAN_POINT ( 'NONE',  ( 10.51115150389377639, 1366.987070946261611, 210.6218459617030021 ) ) ;
#4888=DIRECTION ( 'NONE',  ( -6.123233995736769734E-17, -1.000000000000000000, -1.124819836996399911E-32 ) ) ;
#4890=CARTESIAN_POINT ( 'NONE',  ( -8.126618747047817948, 1364.913278222060626, 208.3718459617061285 ) ) ;
#4990=CARTESIAN_POINT ( 'NONE',  ( -11.03646466085811895, 1367.416071951358845, 208.3718459617010978 ) ) ;
#5019=VERTEX_POINT ( 'NONE', #68457 ) ;
#5126=PLANE ( 'NONE',  #57157 ) ;
#5134=CARTESIAN_POINT ( 'NONE',  ( 8.726849315049999944, 1367.111769039820047, 210.6218459616991936 ) ) ;
#5273=CARTESIAN_POINT ( 'NONE',  ( 7.445922712490000706, 1367.935115748530052, 207.6218459616989946 ) ) ;
#5405=CARTESIAN_POINT ( 'NONE',  ( 5.604365146370000161, 1361.139420828410039, 207.6218459616989946 ) ) ;
#5424=CARTESIAN_POINT ( 'NONE',  ( 11.96845083018959421, 1365.600286352959529, 209.6218459617033432 ) ) ;
#5446=CARTESIAN_POINT ( 'NONE',  ( -8.000269850835890040, 1364.913076074710261, 209.6218459617148824 ) ) ;
#5469=CARTESIAN_POINT ( 'NONE',  ( -2.860398500404036870, 1367.969949366576884, 210.0987907617960104 ) ) ;
#5534=APPLICATION_CONTEXT ( 'automotive_design' ) ;
#5556=CARTESIAN_POINT ( 'NONE',  ( -7.954225986665955261, 1360.049804075227485, 208.3718459617010978 ) ) ;
#5666=CARTESIAN_POINT ( 'NONE',  ( 3.160865630554719807, 1370.358795681657284, 206.6712751011299360 ) ) ;
#5700=CARTESIAN_POINT ( 'NONE',  ( 8.251048879700000782, 1367.474174444410210, 210.6218459616991936 ) ) ;
#5733=CARTESIAN_POINT ( 'NONE',  ( 2.775567936913962086, 1367.641464887947222, 209.1220808601200076 ) ) ;
#5863=CARTESIAN_POINT ( 'NONE',  ( 4.501691961449999724, 1368.956319095359959, 207.6218459616989946 ) ) ;
#5961=CARTESIAN_POINT ( 'NONE',  ( -4.309579507020567135, 1362.750343653446180, 208.3718459617061285 ) ) ;
#5964=EDGE_LOOP ( 'NONE', ( #32970, #90754, #617, #7248 ) ) ;
#5976=CARTESIAN_POINT ( 'NONE',  ( 11.85145339950207521, 1363.709651157501412, 209.6218459617033432 ) ) ;
#5997=CARTESIAN_POINT ( 'NONE',  ( -8.103791294879806983, 1364.808472168752587, 208.3718459617061285 ) ) ;
#6096=CARTESIAN_POINT ( 'NONE',  ( -9.230109932484202417, 1361.837706146139681, 207.6218459616987673 ) ) ;
#6160=DIRECTION ( 'NONE',  ( 1.192122195693504081E-14, -4.372198439846870180E-16, -1.000000000000000000 ) ) ;
#6174=CARTESIAN_POINT ( 'NONE',  ( 3.439747417924114536, 1370.269341356917948, 210.1266736013298555 ) ) ;
#6200=DIRECTION ( 'NONE',  ( 0.1403878024439506045, 0.9900965937346509760, 0.000000000000000000 ) ) ;
#6232=CARTESIAN_POINT ( 'NONE',  ( 10.02176186330000185, 1364.879735892739745, 210.6218459616991936 ) ) ;
#6414=ADVANCED_FACE ( 'NONE', ( #80715 ), #48780, .T. ) ;
#6449=CARTESIAN_POINT ( 'NONE',  ( -3.180365954794715400, 1370.226539215816501, 210.2066197577219100 ) ) ;
#6506=CARTESIAN_POINT ( 'NONE',  ( 9.093835586159539019, 1363.023136421986010, 210.6218459616987957 ) ) ;
#6512=CONICAL_SURFACE ( 'NONE', #45861, 1.000000000000005773, 0.7853981633970000820 ) ;
#6524=CARTESIAN_POINT ( 'NONE',  ( 11.17471672580117925, 1365.463530159558559, 210.6218459617030021 ) ) ;
#6605=CIRCLE ( 'NONE', #72803, 3.000000000000002665 ) ;
#6650=CARTESIAN_POINT ( 'NONE',  ( -9.837816714745258651, 1361.043255431922262, 209.6218459617033432 ) ) ;
#6672=CARTESIAN_POINT ( 'NONE',  ( 5.561733859871847763, 1387.291117539184825, 209.1218459616989946 ) ) ;
#6811=DIRECTION ( 'NONE',  ( -6.123233995736769734E-17, -1.000000000000000000, 7.888609052210119587E-33 ) ) ;
#6932=DIRECTION ( 'NONE',  ( -6.123233995736769734E-17, -1.000000000000000000, -1.124819836996399911E-32 ) ) ;
#7061=CARTESIAN_POINT ( 'NONE',  ( 7.787085240219187909, 1364.374563602181297, 208.3718459617061285 ) ) ;
#7072=CIRCLE ( 'NONE', #21347, 19.90662746966999919 ) ;
#7077=CARTESIAN_POINT ( 'NONE',  ( 11.16357413047867730, 1367.453876867194367, 209.6218459617033432 ) ) ;
#7148=FACE_OUTER_BOUND ( 'NONE', #67438, .T. ) ;
#7211=CARTESIAN_POINT ( 'NONE',  ( -8.082564370841041068, 1362.241991287404062, 210.6218459616991936 ) ) ;
#7248=ORIENTED_EDGE ( 'NONE', *, *, #86288, .F. ) ;
#7478=CARTESIAN_POINT ( 'NONE',  ( 3.005276066433927973, 1369.205039411293910, 210.6218459616987957 ) ) ;
#7605=CARTESIAN_POINT ( 'NONE',  ( 7.875197786978843872, 1364.470992309426492, 208.3718459617061285 ) ) ;
#7609=VERTEX_POINT ( 'NONE', #3590 ) ;
#7619=CARTESIAN_POINT ( 'NONE',  ( 8.653423937789300524, 1367.169888897622059, 210.6218459616991936 ) ) ;
#7636=EDGE_CURVE ( 'NONE', #74254, #40999, #11875, .T. ) ;
#7751=CARTESIAN_POINT ( 'NONE',  ( -8.144230935551448169, 1360.896704102203103, 210.6218459617030021 ) ) ;
#7801=DIRECTION ( 'NONE',  ( 0.6038592750913972518, -0.7071067811868637643, -0.3679048462383240903 ) ) ;
#7831=AXIS2_PLACEMENT_3D ( 'NONE', #92683, #9249, #69734 ) ;
#7871=CARTESIAN_POINT ( 'NONE',  ( -8.538839991170080523, 1362.569232148532137, 210.6218459616987957 ) ) ;
#7903=CARTESIAN_POINT ( 'NONE',  ( -3.000000000000000000, 1374.913060387289988, 209.1218459616989946 ) ) ;
#8001=DIRECTION ( 'NONE',  ( 0.1403900382919506529, 0.9900962767066567860, 0.000000000000000000 ) ) ;
#8023=CARTESIAN_POINT ( 'NONE',  ( 2.724500461543110319, 1367.224846223802842, 209.6218459617148824 ) ) ;
#8088=CARTESIAN_POINT ( 'NONE',  ( -4.371985619807400525, 1370.450432915718920, 208.7651754562319582 ) ) ;
#8147=CARTESIAN_POINT ( 'NONE',  ( 8.520620816894430405, 1363.877202865954587, 207.6218459616988241 ) ) ;
#8161=CARTESIAN_POINT ( 'NONE',  ( 5.215187551926136145, 1368.779556716638126, 210.6218459616991936 ) ) ;
#8202=ORIENTED_EDGE ( 'NONE', *, *, #51511, .T. ) ;
#8229=DIRECTION ( 'NONE',  ( -6.123233995736769734E-17, -1.000000000000000000, -1.124819836996399911E-32 ) ) ;
#8295=CARTESIAN_POINT ( 'NONE',  ( 3.618222164275962882, 1359.470288639974342, 210.6218459617030021 ) ) ;
#8381=EDGE_CURVE ( 'NONE', #39065, #32037, #65646, .T. ) ;
#8414=CARTESIAN_POINT ( 'NONE',  ( -7.132082164984229422, 1362.854272046530468, 207.6218459616988241 ) ) ;
#8422=CARTESIAN_POINT ( 'NONE',  ( -8.723604090509862630, 1369.380824275133136, 208.3718459617010978 ) ) ;
#8423=ADVANCED_FACE ( 'NONE', ( #77210 ), #21383, .T. ) ;
#8561=CARTESIAN_POINT ( 'NONE',  ( 0.9603320758176961958, 1368.656171133117368, 210.4211784721450726 ) ) ;
#8697=CARTESIAN_POINT ( 'NONE',  ( 7.310316353548246049, 1364.149046361921137, 209.6218459617148824 ) ) ;
#8700=ORIENTED_EDGE ( 'NONE', *, *, #104366, .F. ) ;
#8713=CARTESIAN_POINT ( 'NONE',  ( 9.798927948586740655, 1367.783618483544160, 210.6218459617030021 ) ) ;
#8778=UNCERTAINTY_MEASURE_WITH_UNIT (LENGTH_MEASURE( 1.000000000000000082E-05 ), #93807, 'distance_accuracy_value', 'NONE');
#8844=CARTESIAN_POINT ( 'NONE',  ( 1.904758451061700386, 1358.442897800721767, 209.6218459617033432 ) ) ;
#8907=CARTESIAN_POINT ( 'NONE',  ( 3.036227701980231508, 1369.423328382213640, 207.6218459616989378 ) ) ;
#8975=CARTESIAN_POINT ( 'NONE',  ( -9.692061980449999226, 1363.802329763670059, 207.6218459616989946 ) ) ;
#8984=CARTESIAN_POINT ( 'NONE',  ( -8.624710350820000926, 1367.191948709370081, 207.6218459616989946 ) ) ;
#9198=STYLED_ITEM ( 'NONE', ( #94942 ), #110798 ) ;
#9249=DIRECTION ( 'NONE',  ( -4.212667542703050259E-16, 6.855153903361010419E-22, -1.000000000000000000 ) ) ;
#9271=CARTESIAN_POINT ( 'NONE',  ( 9.925983360900000108, 1364.303202023270160, 207.6218459616989946 ) ) ;
#9284=CARTESIAN_POINT ( 'NONE',  ( 8.653423937779999520, 1367.169888897630017, 207.6218459616989946 ) ) ;
#9291=ORIENTED_EDGE ( 'NONE', *, *, #29064, .T. ) ;
#9295=CARTESIAN_POINT ( 'NONE',  ( 3.426613460960000079, 1360.656565846710009, 207.6218459616989946 ) ) ;
#9415=CARTESIAN_POINT ( 'NONE',  ( -4.977374762485336390, 1359.949827183397247, 207.6218459616987673 ) ) ;
#9438=CARTESIAN_POINT ( 'NONE',  ( -9.209502321770001387, 1366.683160837839978, 207.6218459616989946 ) ) ;
#9511=CARTESIAN_POINT ( 'NONE',  ( -2.825698915363265229, 1367.725220571654063, 208.9256954109638968 ) ) ;
#9526=CARTESIAN_POINT ( 'NONE',  ( -6.672014541987599578, 1363.744075657580197, 209.6218459617148824 ) ) ;
#9534=CARTESIAN_POINT ( 'NONE',  ( -8.696701630030000629, 1367.135748871429996, 207.6218459616989946 ) ) ;
#9672=CARTESIAN_POINT ( 'NONE',  ( -3.034926079678203159, 1369.200812461396481, 210.6218459616991936 ) ) ;
#9706=EDGE_LOOP ( 'NONE', ( #64760, #57250, #40275, #29766 ) ) ;
#9813=CARTESIAN_POINT ( 'NONE',  ( 8.063859222158944462, 1365.091964226176060, 208.3718459617061285 ) ) ;
#9828=CARTESIAN_POINT ( 'NONE',  ( 10.33932082004445974, 1368.375147307815269, 209.6218459617033432 ) ) ;
#9840=CARTESIAN_POINT ( 'NONE',  ( -8.082564370840000123, 1362.241991287400197, 207.6218459616989946 ) ) ;
#9963=CARTESIAN_POINT ( 'NONE',  ( -2.380813228419999650, 1360.502616939890004, 207.6218459616989946 ) ) ;
#9968=VERTEX_POINT ( 'NONE', #90816 ) ;
#9989=CARTESIAN_POINT ( 'NONE',  ( -5.236338392940000475, 1368.774323667059889, 207.6218459616989946 ) ) ;
#10065=CARTESIAN_POINT ( 'NONE',  ( -2.941554235803736539, 1368.542299806011442, 210.4699219221472219 ) ) ;
#10081=CARTESIAN_POINT ( 'NONE',  ( -8.572405811665989361, 1363.936666048608004, 207.6218459616988241 ) ) ;
#10090=CARTESIAN_POINT ( 'NONE',  ( -4.517103278720104420, 1368.953374755371897, 210.6218459616991936 ) ) ;
#10229=CARTESIAN_POINT ( 'NONE',  ( -4.533972341721243637, 1368.949167378611946, 210.6218459616991936 ) ) ;
#10320=FACE_OUTER_BOUND ( 'NONE', #84943, .T. ) ;
#10362=CARTESIAN_POINT ( 'NONE',  ( 9.984115569242678845, 1365.258395869462220, 210.6218459616987957 ) ) ;
#10388=CARTESIAN_POINT ( 'NONE',  ( -9.830395177430000686, 1365.769828494180047, 207.6218459616989946 ) ) ;
#10518=CARTESIAN_POINT ( 'NONE',  ( -2.488105171088486500, 1359.506461065921940, 207.6218459616987673 ) ) ;
#10546=CARTESIAN_POINT ( 'NONE',  ( -6.615182365728785818, 1366.249946645814816, 208.3718459617061285 ) ) ;
#10648=CARTESIAN_POINT ( 'NONE',  ( 3.235004757640449924, 1361.842843053408615, 210.6218459617142003 ) ) ;
#10656=CARTESIAN_POINT ( 'NONE',  ( -7.895287119950644694, 1368.828961991272308, 207.6218459616987673 ) ) ;
#10739=CARTESIAN_POINT ( 'NONE',  ( 3.442434976254919565, 1370.269799182473889, 208.1179161451651112 ) ) ;
#10750=EDGE_CURVE ( 'NONE', #437, #93985, #28444, .T. ) ;
#10929=CARTESIAN_POINT ( 'NONE',  ( 8.716989280790679473, 1365.703354663701930, 207.6218459616988241 ) ) ;
#10956=CARTESIAN_POINT ( 'NONE',  ( -7.811405798920000088, 1367.739269854440181, 207.6218459616989946 ) ) ;
#11083=CARTESIAN_POINT ( 'NONE',  ( 9.663424421700000266, 1363.752474719049815, 207.6218459616989946 ) ) ;
#11114=CARTESIAN_POINT ( 'NONE',  ( -7.484392838114925617, 1365.703112302720456, 208.3718459617061285 ) ) ;
#11151=ADVANCED_FACE ( 'NONE', ( #18994 ), #6512, .T. ) ;
#11207=CARTESIAN_POINT ( 'NONE',  ( 3.005276066430000448, 1369.205039411269809, 207.6218459616989946 ) ) ;
#11215=CARTESIAN_POINT ( 'NONE',  ( -11.26659152488946525, 1367.047083354208553, 208.3718459617010978 ) ) ;
#11283=CARTESIAN_POINT ( 'NONE',  ( 3.138931148605959913E-16, 1391.413060387289988, 209.1218459616989946 ) ) ;
#11335=CARTESIAN_POINT ( 'NONE',  ( 3.160865630554719807, 1370.358795681657284, 206.6712751011299360 ) ) ;
#11354=CARTESIAN_POINT ( 'NONE',  ( -5.247433916391508468, 1368.770886448055307, 210.6218459616991936 ) ) ;
#11445=FACE_OUTER_BOUND ( 'NONE', #63874, .T. ) ;
#11484=CARTESIAN_POINT ( 'NONE',  ( 7.427103032054851894, 1365.589452326314131, 209.6218459617148824 ) ) ;
#11510=CARTESIAN_POINT ( 'NONE',  ( -9.936738324559998503, 1364.340818343090177, 207.6218459616989946 ) ) ;
#11626=CARTESIAN_POINT ( 'NONE',  ( 7.340269731169999368, 1361.836778001489847, 207.6218459616989946 ) ) ;
#11648=CARTESIAN_POINT ( 'NONE',  ( -8.624710350826600092, 1367.191948709382132, 210.6218459616987957 ) ) ;
#11748=CARTESIAN_POINT ( 'NONE',  ( -9.936738324559998503, 1364.340818343090177, 207.6218459616989946 ) ) ;
#11832=CARTESIAN_POINT ( 'NONE',  ( 4.370200466702017117, 1370.450046576546811, 208.7619599720994472 ) ) ;
#11875=CIRCLE ( 'NONE', #92265, 8.989690721650012151 ) ;
#11949=FACE_OUTER_BOUND ( 'NONE', #36032, .T. ) ;
#12025=CARTESIAN_POINT ( 'NONE',  ( 4.239534266359169301, 1367.783695315041314, 210.6218459617142003 ) ) ;
#12083=ADVANCED_FACE ( 'NONE', ( #56651 ), #61165, .T. ) ;
#12111=DIRECTION ( 'NONE',  ( 0.9900965937346509760, 0.1403878024439500216, 3.790652827686680047E-16 ) ) ;
#12167=CARTESIAN_POINT ( 'NONE',  ( 8.796059898601679805, 1362.759824263854171, 210.6218459616991936 ) ) ;
#12189=CARTESIAN_POINT ( 'NONE',  ( -8.706062076307372166, 1365.718773072405384, 207.6218459616988241 ) ) ;
#12215=CIRCLE ( 'NONE', #74823, 17.26401014167801762 ) ;
#12216=CARTESIAN_POINT ( 'NONE',  ( 8.775825618903722258, 1374.031200045389824, 213.9161013477410336 ) ) ;
#12284=CARTESIAN_POINT ( 'NONE',  ( -11.95743746174541933, 1364.171459020583370, 209.6218459617033432 ) ) ;
#12297=AXIS2_PLACEMENT_3D ( 'NONE', #11283, #18539, #104776 ) ;
#12354=DIRECTION ( 'NONE',  ( 6.123233995736769734E-17, 1.000000000000000000, 1.124819836996399911E-32 ) ) ;
#12364=CIRCLE ( 'NONE', #67776, 0.4999999999999980016 ) ;
#12369=CARTESIAN_POINT ( 'NONE',  ( 4.459680871607520913, 1370.469415166398903, 208.9741522785391510 ) ) ;
#12423=CARTESIAN_POINT ( 'NONE',  ( 2.632747685671116056, 1389.413060387289988, 210.5601225775116063 ) ) ;
#12432=CARTESIAN_POINT ( 'NONE',  ( 9.258247136800001442, 1363.198586359130104, 210.6218459616991936 ) ) ;
#12498=DIRECTION ( 'NONE',  ( -1.000000000000000000, 6.123233995736769734E-17, 0.000000000000000000 ) ) ;
#12576=CARTESIAN_POINT ( 'NONE',  ( 8.100491796851672532, 1366.331969060035135, 207.6218459616988241 ) ) ;
#12591=DIRECTION ( 'NONE',  ( -1.407418274235000032E-17, -1.000000000000000000, 2.576261870300899651E-17 ) ) ;
#12668=DIRECTION ( 'NONE',  ( -0.1403878024439498828, 0.9900965937346509760, 0.000000000000000000 ) ) ;
#12706=CARTESIAN_POINT ( 'NONE',  ( -4.466366219213330879, 1362.092831090860955, 210.6218459617142003 ) ) ;
#12725=CARTESIAN_POINT ( 'NONE',  ( 11.03759844033949911, 1362.198095653763176, 209.6218459617033432 ) ) ;
#12748=CARTESIAN_POINT ( 'NONE',  ( -7.895487264294541063, 1365.128408244944467, 209.6218459617148824 ) ) ;
#12749=ORIENTED_EDGE ( 'NONE', *, *, #86288, .T. ) ;
#12814=ORIENTED_EDGE ( 'NONE', *, *, #36890, .F. ) ;
#12841=CARTESIAN_POINT ( 'NONE',  ( -11.67741975794039178, 1363.266342174300917, 209.6218459617033432 ) ) ;
#12843=CARTESIAN_POINT ( 'NONE',  ( 3.071538966616301103, 1374.913060387290216, 210.7998353468136941 ) ) ;
#12879=( NAMED_UNIT ( * ) SI_UNIT ( $, .STERADIAN. ) SOLID_ANGLE_UNIT ( ) );
#12972=CARTESIAN_POINT ( 'NONE',  ( -7.592149787969999508, 1361.964468435470053, 210.6218459616991936 ) ) ;
#13100=CARTESIAN_POINT ( 'NONE',  ( 7.503748088656135629, 1365.688229612017949, 208.3718459617061285 ) ) ;
#13234=CARTESIAN_POINT ( 'NONE',  ( -2.166229343104828509, 1362.494928687810898, 209.6218459617148824 ) ) ;
#13249=CARTESIAN_POINT ( 'NONE',  ( 7.877099145829919991, 1362.118768394185963, 210.6218459616991936 ) ) ;
#13273=CARTESIAN_POINT ( 'NONE',  ( -8.909267011570118910, 1365.369432761979624, 207.6218459616988241 ) ) ;
#13279=CARTESIAN_POINT ( 'NONE',  ( 2.724500461545519059, 1367.224846223802842, 209.6218459617149108 ) ) ;
#13326=DIRECTION ( 'NONE',  ( 0.9900965937346507539, -0.1403878024439509931, 3.790652827686679061E-16 ) ) ;
#13374=CARTESIAN_POINT ( 'NONE',  ( -9.977700672470000143, 1365.292605733890014, 207.6218459616989946 ) ) ;
#13443=ORIENTED_EDGE ( 'NONE', *, *, #3019, .T. ) ;
#13514=CARTESIAN_POINT ( 'NONE',  ( 4.262353028400000632, 1360.811275533930029, 210.6218459616991936 ) ) ;
#13643=CARTESIAN_POINT ( 'NONE',  ( 8.988338641415380081, 1366.896325247159893, 210.6218459616987957 ) ) ;
#13688=ADVANCED_FACE ( 'NONE', ( #58277 ), #85657, .T. ) ;
#13783=CARTESIAN_POINT ( 'NONE',  ( 4.058282819955586262, 1361.791725152615072, 207.6218459616988241 ) ) ;
#13799=CARTESIAN_POINT ( 'NONE',  ( 11.91688765630230762, 1364.847998537791682, 208.3718459617010978 ) ) ;
#13801=ORIENTED_EDGE ( 'NONE', *, *, #106154, .T. ) ;
#13823=CARTESIAN_POINT ( 'NONE',  ( -8.774526971944801801, 1365.153596817209063, 210.6218459617142003 ) ) ;
#13844=ORIENTED_EDGE ( 'NONE', *, *, #82806, .T. ) ;
#13929=CARTESIAN_POINT ( 'NONE',  ( -9.328535443848540609, 1363.278783432131831, 210.6218459616991936 ) ) ;
#14055=CONICAL_SURFACE ( 'NONE', #12297, 1.000000000000005773, 0.7853981633970000820 ) ;
#14067=CARTESIAN_POINT ( 'NONE',  ( 8.272555700608019129E-16, 1374.413060387289988, 209.1218459616989946 ) ) ;
#14249=EDGE_CURVE ( 'NONE', #7609, #74455, #62439, .T. ) ;
#14251=ORIENTED_EDGE ( 'NONE', *, *, #17933, .T. ) ;
#14341=CARTESIAN_POINT ( 'NONE',  ( 4.017468778259492446, 1361.987815076348852, 210.6218459617142003 ) ) ;
#14357=CARTESIAN_POINT ( 'NONE',  ( 9.663424421699261302, 1363.752474719050042, 210.6218459616991936 ) ) ;
#14380=CARTESIAN_POINT ( 'NONE',  ( -10.02185219043178144, 1364.916310432309956, 210.6218459616987957 ) ) ;
#14487=CARTESIAN_POINT ( 'NONE',  ( -9.692061980449999226, 1363.802329763670059, 207.6218459616989946 ) ) ;
#14593=ORIENTED_EDGE ( 'NONE', *, *, #23305, .T. ) ;
#14631=CARTESIAN_POINT ( 'NONE',  ( -4.745098151930000618, 1360.923919868589792, 210.6218459616991936 ) ) ;
#14852=DIRECTION ( 'NONE',  ( -6.123233995736769734E-17, -1.000000000000000000, -1.124819836996399911E-32 ) ) ;
#14858=ORIENTED_EDGE ( 'NONE', *, *, #3019, .F. ) ;
#14891=CARTESIAN_POINT ( 'NONE',  ( 7.243489813520766596, 1364.101810452927566, 209.6218459617148824 ) ) ;
#14907=CARTESIAN_POINT ( 'NONE',  ( 11.52816579256459306, 1363.237826914502875, 208.3718459617010978 ) ) ;
#15027=CARTESIAN_POINT ( 'NONE',  ( -9.761853366963894274, 1361.142561771200917, 208.3718459617010978 ) ) ;
#15221=FACE_OUTER_BOUND ( 'NONE', #27620, .T. ) ;
#15308=CARTESIAN_POINT ( 'NONE',  ( 3.577843379407391833, 1368.113851476867239, 207.6218459616988241 ) ) ;
#15341=DIRECTION ( 'NONE',  ( -0.1403878024439498828, 0.9900965937346509760, 0.000000000000000000 ) ) ;
#15378=CARTESIAN_POINT ( 'NONE',  ( -4.125989513582625889, 1370.398720948539221, 208.4821978858626892 ) ) ;
#15438=CARTESIAN_POINT ( 'NONE',  ( 8.379275254590000443, 1362.454991452509830, 207.6218459616989946 ) ) ;
#15454=CARTESIAN_POINT ( 'NONE',  ( 11.81974299095224801, 1364.123681825266203, 208.3718459617010978 ) ) ;
#15478=ORIENTED_EDGE ( 'NONE', *, *, #109804, .F. ) ;
#15530=VECTOR ( 'NONE', #7801, 999.9999999999998863 ) ;
#15572=CARTESIAN_POINT ( 'NONE',  ( -9.122811643198552645, 1360.526723316428388, 209.6218459617033432 ) ) ;
#15602=AXIS2_PLACEMENT_3D ( 'NONE', #17025, #68594, #93748 ) ;
#15635=CARTESIAN_POINT ( 'NONE',  ( -2.603248992506880022, 1366.156374083119999, 209.1218459584009963 ) ) ;
#15693=ADVANCED_FACE ( 'NONE', ( #7148 ), #36025, .T. ) ;
#15845=CARTESIAN_POINT ( 'NONE',  ( 3.005276066430000448, 1369.205039411269809, 207.6218459616989946 ) ) ;
#15932=AXIS2_PLACEMENT_3D ( 'NONE', #76388, #94848, #33825 ) ;
#15971=VERTEX_POINT ( 'NONE', #56604 ) ;
#15985=CARTESIAN_POINT ( 'NONE',  ( 7.523183757958989304, 1364.306666347853707, 209.6218459617148824 ) ) ;
#16001=CARTESIAN_POINT ( 'NONE',  ( 9.532517564019999057, 1366.286862064870093, 207.6218459616989946 ) ) ;
#16132=CARTESIAN_POINT ( 'NONE',  ( -8.910387285849060035, 1362.858511851213962, 210.6218459616991936 ) ) ;
#16183=CARTESIAN_POINT ( 'NONE',  ( 0.8539859765994233243, 1391.413060387289988, 208.6015499384857321 ) ) ;
#16234=CARTESIAN_POINT ( 'NONE',  ( -6.123233995736771213E-16, 1379.913060387289988, 209.1218459616989946 ) ) ;
#16251=CARTESIAN_POINT ( 'NONE',  ( -9.655745333052619728, 1363.739547551583883, 210.6218459616987957 ) ) ;
#16283=FACE_OUTER_BOUND ( 'NONE', #101099, .T. ) ;
#16292=DIRECTION ( 'NONE',  ( 0.1403901532130616969, 0.9900962604114879051, 0.000000000000000000 ) ) ;
#16466=CARTESIAN_POINT ( 'NONE',  ( -4.473512919476954508, 1370.472450005593828, 209.0513769001518654 ) ) ;
#16526=CARTESIAN_POINT ( 'NONE',  ( 8.776071739740523014, 1364.218562676873489, 207.6218459616988241 ) ) ;
#16539=CARTESIAN_POINT ( 'NONE',  ( 5.705396399765596094, 1370.592093591774528, 208.3718459617010978 ) ) ;
#16672=CARTESIAN_POINT ( 'NONE',  ( 3.745961299822565760, 1358.679437168825416, 209.6218459617033432 ) ) ;
#16694=ORIENTED_EDGE ( 'NONE', *, *, #63923, .F. ) ;
#16771=ORIENTED_EDGE ( 'NONE', *, *, #102365, .T. ) ;
#16792=CARTESIAN_POINT ( 'NONE',  ( -8.538839991170000587, 1362.569232148550100, 207.6218459616989946 ) ) ;
#16801=CARTESIAN_POINT ( 'NONE',  ( -4.517103279549999684, 1368.953374755989898, 207.6218459616989946 ) ) ;
#17025=CARTESIAN_POINT ( 'NONE',  ( -1.331958139231829923E-15, 1375.413060387289988, 209.1218459616989946 ) ) ;
#17069=CARTESIAN_POINT ( 'NONE',  ( 8.796059898609998484, 1362.759824263850078, 207.6218459616989946 ) ) ;
#17088=CARTESIAN_POINT ( 'NONE',  ( 4.501691961672608322, 1368.956319095223989, 210.6218459616991936 ) ) ;
#17221=CARTESIAN_POINT ( 'NONE',  ( 5.604365146379768348, 1361.139420828405946, 210.6218459616991936 ) ) ;
#17287=DIRECTION ( 'NONE',  ( -0.1215789942062150408, 0.8574459172214612401, -0.5000050471825780996 ) ) ;
#17346=CARTESIAN_POINT ( 'NONE',  ( -7.945335120643528093, 1363.374344492768842, 207.6218459616988241 ) ) ;
#17355=CARTESIAN_POINT ( 'NONE',  ( -8.962252599310001955, 1366.920250605820002, 207.6218459616989946 ) ) ;
#17424=ORIENTED_EDGE ( 'NONE', *, *, #60483, .F. ) ;
#17477=CARTESIAN_POINT ( 'NONE',  ( -0.01912617869007780455, 1347.932019967219958, 212.1218459616989946 ) ) ;
#17630=CARTESIAN_POINT ( 'NONE',  ( 9.943976501859779660, 1365.461622992602088, 210.6218459616987957 ) ) ;
#17633=EDGE_LOOP ( 'NONE', ( #88361, #88623, #64220, #48147, #8202 ) ) ;
#17648=CARTESIAN_POINT ( 'NONE',  ( 8.731474709677369717, 1369.377627139728020, 208.3718459617010978 ) ) ;
#17779=CARTESIAN_POINT ( 'NONE',  ( -2.595397113752544449, 1358.510305191965017, 209.6218459617033432 ) ) ;
#17848=ADVANCED_FACE ( 'NONE', ( #15221 ), #24173, .T. ) ;
#17851=CIRCLE ( 'NONE', #103729, 17.26401014167801762 ) ;
#17891=CARTESIAN_POINT ( 'NONE',  ( -2.906570293435709385, 1368.295572657563525, 210.3150243549862068 ) ) ;
#17901=EDGE_CURVE ( 'NONE', #40999, #97580, #65695, .T. ) ;
#17908=CARTESIAN_POINT ( 'NONE',  ( -7.458416007436354356, 1363.271152069968139, 210.6218459617142003 ) ) ;
#17917=CARTESIAN_POINT ( 'NONE',  ( -5.761781897038445344, 1370.707051359383968, 209.6218459617033432 ) ) ;
#17933=EDGE_CURVE ( 'NONE', #66318, #60506, #69217, .T. ) ;
#17967=EDGE_CURVE ( 'NONE', #93985, #25781, #3131, .T. ) ;
#18113=EDGE_CURVE ( 'NONE', #78057, #69033, #6605, .T. ) ;
#18150=VERTEX_POINT ( 'NONE', #75588 ) ;
#18154=EDGE_CURVE ( 'NONE', #32551, #1227, #24027, .T. ) ;
#18200=CARTESIAN_POINT ( 'NONE',  ( 8.778479041704853714, 1365.138727624712828, 210.6218459617142003 ) ) ;
#18213=CARTESIAN_POINT ( 'NONE',  ( 6.697942107255492772, 1369.372287355299250, 207.6218459616987673 ) ) ;
#18224=CARTESIAN_POINT ( 'NONE',  ( 9.813910351400000565, 1364.017814053650000, 207.6218459616989946 ) ) ;
#18237=DIRECTION ( 'NONE',  ( -6.123233995736769734E-17, -1.000000000000000000, -1.124819836996399911E-32 ) ) ;
#18343=CARTESIAN_POINT ( 'NONE',  ( 0.06326327880447388252, 1358.388637432561609, 209.6218459617033432 ) ) ;
#18367=CARTESIAN_POINT ( 'NONE',  ( -5.690168351895294130, 1366.535003315410449, 209.6218459617148824 ) ) ;
#18399=CARTESIAN_POINT ( 'NONE',  ( 3.097576048983416541, 1369.855992675987409, 207.7442862697458565 ) ) ;
#18456=CARTESIAN_POINT ( 'NONE',  ( -9.178315062050000250, 1363.109187794150102, 207.6218459616989946 ) ) ;
#18465=CARTESIAN_POINT ( 'NONE',  ( -9.765027863526395180, 1368.680785116012430, 208.3718459617010978 ) ) ;
#18507=SURFACE_SIDE_STYLE ('',( #27477 ) ) ;
#18524=DIRECTION ( 'NONE',  ( -0.8775825618903723147, 0.000000000000000000, -0.4794255386042039491 ) ) ;
#18539=DIRECTION ( 'NONE',  ( -5.053215498073659967E-16, -1.000000000000000000, -2.442490654180000246E-15 ) ) ;
#18569=DIRECTION ( 'NONE',  ( 0.4794255386042041156, -5.511896626706601104E-17, -0.8775825618903722036 ) ) ;
#18746=CARTESIAN_POINT ( 'NONE',  ( 7.999780308251754235, 1364.916505385960136, 209.6218459617148824 ) ) ;
#18895=CARTESIAN_POINT ( 'NONE',  ( -2.509563559622638884, 1359.307229891140196, 210.6218459617030021 ) ) ;
#18919=CARTESIAN_POINT ( 'NONE',  ( -7.706043838548156444, 1365.524518540627469, 208.3718459617061285 ) ) ;
#18994=FACE_OUTER_BOUND ( 'NONE', #20016, .T. ) ;
#19010=CARTESIAN_POINT ( 'NONE',  ( 1.748848150589999983, 1360.440694539920059, 207.6218459616989946 ) ) ;
#19018=CARTESIAN_POINT ( 'NONE',  ( -4.955698549128424446, 1370.907435100005841, 209.6218459617033432 ) ) ;
#19075=CARTESIAN_POINT ( 'NONE',  ( -5.599233173528683771, 1387.285800435509827, 209.1218459616989946 ) ) ;
#19154=CARTESIAN_POINT ( 'NONE',  ( 2.986193535308999891, 1369.126893976419979, 209.1220808601199792 ) ) ;
#19156=CARTESIAN_POINT ( 'NONE',  ( -9.692061980449999226, 1363.802329763670059, 210.6218459616991936 ) ) ;
#19299=CARTESIAN_POINT ( 'NONE',  ( 8.000513322313473452, 1364.896752889035270, 209.6218459617148824 ) ) ;
#19324=CARTESIAN_POINT ( 'NONE',  ( 9.925983360900000108, 1364.303202023270160, 207.6218459616989946 ) ) ;
#19347=EDGE_CURVE ( 'NONE', #93985, #437, #105082, .T. ) ;
#19412=AXIS2_PLACEMENT_3D ( 'NONE', #91274, #6160, #32480 ) ;
#19455=CARTESIAN_POINT ( 'NONE',  ( 11.31426556939452510, 1362.616033936885287, 209.6218459617033432 ) ) ;
#19482=CARTESIAN_POINT ( 'NONE',  ( -7.581703558749627980, 1366.473201395314163, 210.6218459617142003 ) ) ;
#19580=CARTESIAN_POINT ( 'NONE',  ( -0.7279988002571550210, 1361.403840689056096, 207.6218459616988241 ) ) ;
#19587=CARTESIAN_POINT ( 'NONE',  ( -10.96801198806809374, 1364.355713703397896, 207.6218459616987673 ) ) ;
#19683=ADVANCED_FACE ( 'NONE', ( #77537 ), #28200, .F. ) ;
#19861=CARTESIAN_POINT ( 'NONE',  ( 8.448716945488873975, 1365.724340617022563, 210.6218459617142003 ) ) ;
#19884=CARTESIAN_POINT ( 'NONE',  ( -9.657355732020000971, 1366.083296228050131, 207.6218459616989946 ) ) ;
#20014=CARTESIAN_POINT ( 'NONE',  ( 11.27652648530197510, 1362.794758922350184, 208.3718459617010978 ) ) ;
#20016=EDGE_LOOP ( 'NONE', ( #2192, #4578, #108481, #85573, #86270 ) ) ;
#20037=CARTESIAN_POINT ( 'NONE',  ( -8.339847315937356953, 1365.851959156268776, 210.6218459617142003 ) ) ;
#20138=CARTESIAN_POINT ( 'NONE',  ( -9.936738324538698208, 1364.340818343091769, 210.6218459616991936 ) ) ;
#20404=CARTESIAN_POINT ( 'NONE',  ( 7.597707828889148196, 1366.463672655298296, 210.6218459617142003 ) ) ;
#20419=CARTESIAN_POINT ( 'NONE',  ( 3.268503196014072465, 1371.061470524529796, 208.3718459617010978 ) ) ;
#20549=CARTESIAN_POINT ( 'NONE',  ( 9.622136349630000751, 1363.684386430210225, 207.6218459616989946 ) ) ;
#20567=VECTOR ( 'NONE', #107059, 1000.000000000000000 ) ;
#20572=CARTESIAN_POINT ( 'NONE',  ( -9.692061980470359828, 1363.802329763660055, 210.6218459616987957 ) ) ;
#20661=ORIENTED_EDGE ( 'NONE', *, *, #19347, .T. ) ;
#20673=CARTESIAN_POINT ( 'NONE',  ( -11.09819096161026408, 1364.005208992933603, 210.6218459617030021 ) ) ;
#20714=( NAMED_UNIT ( * ) PLANE_ANGLE_UNIT ( ) SI_UNIT ( $, .RADIAN. ) );
#20823=CARTESIAN_POINT ( 'NONE',  ( 4.501691961669999742, 1368.956319095230128, 210.6218459616991936 ) ) ;
#20954=CARTESIAN_POINT ( 'NONE',  ( 7.552428968428530176, 1365.649644077722996, 208.3718459617061285 ) ) ;
#21040=CARTESIAN_POINT ( 'NONE',  ( -5.599233173528683771, 1387.285800435509827, 209.1218459616989946 ) ) ;
#21098=CARTESIAN_POINT ( 'NONE',  ( 8.476942927298200203, 1362.523913559719858, 210.6218459616991936 ) ) ;
#21118=CARTESIAN_POINT ( 'NONE',  ( -7.999735567014255366, 1364.908477751830560, 209.6218459617148824 ) ) ;
#21209=CARTESIAN_POINT ( 'NONE',  ( -10.90461552211807295, 1364.061143884626290, 207.6218459616987673 ) ) ;
#21295=CARTESIAN_POINT ( 'NONE',  ( 4.401912331127000755, 1370.456889401766148, 209.4259416260188686 ) ) ;
#21347=AXIS2_PLACEMENT_3D ( 'NONE', #100964, #41073, #109400 ) ;
#21358=CARTESIAN_POINT ( 'NONE',  ( 6.892224678229999846, 1361.632554499760090, 210.6218459616991936 ) ) ;
#21383=( BOUNDED_SURFACE ( )  B_SPLINE_SURFACE ( 5, 5, ( 
 ( #43053, #31466, #513, #57802, #39326, #34638 ),
 ( #40418, #68822, #102923, #32022, #26223, #60412 ),
 ( #97301, #53117, #78871, #44159, #77753, #43602 ),
 ( #2177, #86695, #3275, #1062, #104605, #9989 ),
 ( #36292, #105725, #18367, #71604, #27898, #87254 ),
 ( #54232, #52562, #35190, #10546, #36847, #45275 ),
 ( #78296, #88359, #62081, #96207, #70485, #1609 ),
 ( #95652, #19482, #53685, #44719, #79413, #69933 ),
 ( #11648, #87826, #35746, #11114, #104046, #27338 ),
 ( #61524, #62646, #2725, #71039, #29009, #45825 ),
 ( #105160, #28452, #79958, #18919, #96768, #63194 ),
 ( #37405, #20037, #52005, #86145, #103483, #9438 ),
 ( #69374, #26788, #60976, #95101, #22218, #106794 ),
 ( #21671, #47465, #12748, #46382, #12189, #39031 ),
 ( #55323, #82708, #40149, #80514, #63730, #3831 ),
 ( #72668, #88903, #74332, #22766, #89998, #30084 ),
 ( #30650, #56970, #64278, #37959, #13273, #81586 ),
 ( #72140, #13823, #31742, #106257, #64836, #55877 ),
 ( #48009, #98943, #73776, #38491, #56416, #29543 ),
 ( #14380, #48573, #5446, #4890, #39606, #46930 ),
 ( #97840, #98398, #21118, #73210, #90546, #107900 ),
 ( #89455, #107354, #81048, #31193, #4363, #91102 ),
 ( #82147, #65380, #99483, #5997, #108460, #65929 ),
 ( #20572, #54771, #101917, #42038, #50, #8975 ),
 ( #16251, #26891, #67806, #68922, #43147, #86791 ),
 ( #34731, #76739, #25206, #34181, #94077, #77304 ),
 ( #26318, #35848, #60510, #1708, #10081, #68366 ),
 ( #92978, #94634, #95196, #76190, #103022, #18456 ),
 ( #35286, #102473, #25763, #70033, #59962, #51542 ),
 ( #50455, #84579, #602, #85679, #59410, #44256 ),
 ( #7871, #93523, #110337, #33609, #17346, #16792 ),
 ( #50996, #17908, #52105, #42586, #86235, #69471 ),
 ( #85126, #61081, #9526, #43694, #8414, #78398 ),
 ( #77847, #1156, #103591, #58844, #52654, #24644 ),
 ( #87919, #104694, #56926, #70577, #2274, #27989 ),
 ( #53211, #12706, #38994, #5961, #47423, #39565 ),
 ( #95746, #96300, #78969, #81015, #36388, #81546 ),
 ( #82107, #4847, #13234, #107861, #62174, #73171 ),
 ( #30046, #87352, #48531, #91055, #19580, #22176 ),
 ( #72624, #107315, #106756, #22724, #82670, #53782 ),
 ( #30610, #64238, #99447, #31150, #46889, #19010 ),
 ( #98906, #10648, #4321, #65338, #64797, #56375 ),
 ( #38452, #14341, #98360, #90505, #13783, #21633 ),
 ( #89959, #47965, #44815, #40106, #55838, #5405 ),
 ( #73738, #104145, #27430, #61613, #110070, #66985 ),
 ( #76468, #49630, #32801, #33346, #110621, #41216 ),
 ( #93795, #109525, #101642, #74833, #102211, #58580 ),
 ( #67541, #33903, #14891, #41759, #68098, #15438 ),
 ( #75388, #83765, #8697, #101096, #24395, #66443 ),
 ( #65885, #92709, #15985, #108976, #25492, #17069 ),
 ( #6506, #57490, #100005, #7061, #31702, #51266 ),
 ( #50188, #84314, #92167, #7605, #8147, #59682 ),
 ( #85399, #75918, #24930, #91614, #74288, #32263 ),
 ( #59140, #100558, #108418, #93263, #16526, #50717 ),
 ( #23293, #49082, #83217, #40660, #84846, #42313 ),
 ( #23838, #58030, #85971, #60802, #102744, #35562 ),
 ( #61909, #87078, #19299, #70317, #26039, #9271 ),
 ( #95479, #889, #60232, #103875, #78118, #26606 ),
 ( #104984, #43431, #51834, #77580, #94928, #94351 ),
 ( #10362, #54064, #18746, #87643, #68644, #34467 ),
 ( #17630, #18200, #35011, #52940, #69192, #53499 ),
 ( #103298, #52397, #27176, #96590, #86520, #62469 ),
 ( #43981, #36678, #45105, #9813, #1422, #69759 ),
 ( #36132, #61360, #44535, #79245, #78680, #1997 ),
 ( #104430, #2555, #27723, #96027, #10929, #70871 ),
 ( #28274, #19861, #88191, #42877, #77034, #342 ),
 ( #88741, #38316, #106086, #22038, #47283, #4183 ),
 ( #13643, #97680, #80888, #81406, #47833, #89280 ),
 ( #4718, #99312, #107734, #20954, #12576, #30471 ),
 ( #55158, #22585, #11484, #13100, #56790, #97135 ),
 ( #46757, #20404, #72495, #106624, #3656, #81966 ),
 ( #29911, #64104, #46205, #73605, #31019, #3104 ),
 ( #105546, #37233, #63565, #79798, #65199, #5273 ),
 ( #98224, #29364, #21494, #39429, #55707, #28833 ),
 ( #89827, #71430, #63030, #38862, #45660, #54609 ),
 ( #73040, #12025, #107181, #64658, #98776, #80340 ),
 ( #56236, #90365, #37786, #71974, #15308, #110492 ),
 ( #7478, #91489, #8023, #75256, #48399, #15845 ) ),
 .UNSPECIFIED., .F., .F., .T. ) 
 B_SPLINE_SURFACE_WITH_KNOTS ( ( 6, 3, 3, 3, 3, 3, 3, 3, 3, 3, 3, 3, 3, 3, 3, 3, 3, 3, 3, 3, 3, 3, 3, 3, 3, 6 ),
 ( 6, 6 ),
 ( 0.000000000000000000, 3.902585213099999617, 6.240861926940000082, 6.790072646649999655, 8.377982366400001268, 8.928580102349998882, 10.97133995140000096, 12.98949692180000071, 13.60228008900000063, 15.24737252870000148, 15.86745694640000082, 18.51059426890000026, 22.57641725190000059, 26.75087197450000076, 31.16005629229999840, 33.90953505430000092, 34.60237748540000524, 36.31249047570000243, 36.97255805550000218, 38.99052022429999909, 41.04947707190000017, 41.62972334150000364, 43.19545136810000230, 43.76106149099999953, 46.17824368760000198, 50.04091111600000374 ),
 ( 4.712388980370019631, 9.424777960769999297 ),
 .UNSPECIFIED. ) 
 GEOMETRIC_REPRESENTATION_ITEM ( )  RATIONAL_B_SPLINE_SURFACE ( (
 ( 0.2500000000000000000, 0.2499999999993640087, 0.2999999999990460298, 0.3999999999987279842, 0.5999999999987279953, 1.000000000000000000),
 ( 0.2500000000000000000, 0.2499999999993640087, 0.2999999999990460298, 0.3999999999987279842, 0.5999999999987279953, 1.000000000000000000),
 ( 0.2500000000000000000, 0.2499999999993640087, 0.2999999999990460298, 0.3999999999987279842, 0.5999999999987279953, 1.000000000000000000),
 ( 0.2500000000000000000, 0.2499999999993640087, 0.2999999999990460298, 0.3999999999987279842, 0.5999999999987279953, 1.000000000000000000),
 ( 0.2500000000000000000, 0.2499999999993640087, 0.2999999999990460298, 0.3999999999987279842, 0.5999999999987279953, 1.000000000000000000),
 ( 0.2500000000000000000, 0.2499999999993640087, 0.2999999999990460298, 0.3999999999987279842, 0.5999999999987279953, 1.000000000000000000),
 ( 0.2500000000000000000, 0.2499999999993640087, 0.2999999999990460298, 0.3999999999987279842, 0.5999999999987279953, 1.000000000000000000),
 ( 0.2500000000000000000, 0.2499999999993640087, 0.2999999999990460298, 0.3999999999987279842, 0.5999999999987279953, 1.000000000000000000),
 ( 0.2500000000000000000, 0.2499999999993640087, 0.2999999999990460298, 0.3999999999987279842, 0.5999999999987279953, 1.000000000000000000),
 ( 0.2500000000000000000, 0.2499999999993640087, 0.2999999999990460298, 0.3999999999987279842, 0.5999999999987279953, 1.000000000000000000),
 ( 0.2500000000000000000, 0.2499999999993640087, 0.2999999999990460298, 0.3999999999987279842, 0.5999999999987279953, 1.000000000000000000),
 ( 0.2500000000000000000, 0.2499999999993640087, 0.2999999999990460298, 0.3999999999987279842, 0.5999999999987279953, 1.000000000000000000),
 ( 0.2500000000000000000, 0.2499999999993640087, 0.2999999999990460298, 0.3999999999987279842, 0.5999999999987279953, 1.000000000000000000),
 ( 0.2500000000000000000, 0.2499999999993640087, 0.2999999999990460298, 0.3999999999987279842, 0.5999999999987279953, 1.000000000000000000),
 ( 0.2500000000000000000, 0.2499999999993640087, 0.2999999999990460298, 0.3999999999987279842, 0.5999999999987279953, 1.000000000000000000),
 ( 0.2500000000000000000, 0.2499999999993640087, 0.2999999999990460298, 0.3999999999987279842, 0.5999999999987279953, 1.000000000000000000),
 ( 0.2500000000000000000, 0.2499999999993640087, 0.2999999999990460298, 0.3999999999987279842, 0.5999999999987279953, 1.000000000000000000),
 ( 0.2500000000000000000, 0.2499999999993640087, 0.2999999999990460298, 0.3999999999987279842, 0.5999999999987279953, 1.000000000000000000),
 ( 0.2500000000000000000, 0.2499999999993640087, 0.2999999999990460298, 0.3999999999987279842, 0.5999999999987279953, 1.000000000000000000),
 ( 0.2500000000000000000, 0.2499999999993640087, 0.2999999999990460298, 0.3999999999987279842, 0.5999999999987279953, 1.000000000000000000),
 ( 0.2500000000000000000, 0.2499999999993640087, 0.2999999999990460298, 0.3999999999987279842, 0.5999999999987279953, 1.000000000000000000),
 ( 0.2500000000000000000, 0.2499999999993640087, 0.2999999999990460298, 0.3999999999987279842, 0.5999999999987279953, 1.000000000000000000),
 ( 0.2500000000000000000, 0.2499999999993640087, 0.2999999999990460298, 0.3999999999987279842, 0.5999999999987279953, 1.000000000000000000),
 ( 0.2500000000000000000, 0.2499999999993640087, 0.2999999999990460298, 0.3999999999987279842, 0.5999999999987279953, 1.000000000000000000),
 ( 0.2500000000000000000, 0.2499999999993640087, 0.2999999999990460298, 0.3999999999987279842, 0.5999999999987279953, 1.000000000000000000),
 ( 0.2500000000000000000, 0.2499999999993640087, 0.2999999999990460298, 0.3999999999987279842, 0.5999999999987279953, 1.000000000000000000),
 ( 0.2500000000000000000, 0.2499999999993640087, 0.2999999999990460298, 0.3999999999987279842, 0.5999999999987279953, 1.000000000000000000),
 ( 0.2500000000000000000, 0.2499999999993640087, 0.2999999999990460298, 0.3999999999987279842, 0.5999999999987279953, 1.000000000000000000),
 ( 0.2500000000000000000, 0.2499999999993640087, 0.2999999999990460298, 0.3999999999987279842, 0.5999999999987279953, 1.000000000000000000),
 ( 0.2500000000000000000, 0.2499999999993640087, 0.2999999999990460298, 0.3999999999987279842, 0.5999999999987279953, 1.000000000000000000),
 ( 0.2500000000000000000, 0.2499999999993640087, 0.2999999999990460298, 0.3999999999987279842, 0.5999999999987279953, 1.000000000000000000),
 ( 0.2500000000000000000, 0.2499999999993640087, 0.2999999999990460298, 0.3999999999987279842, 0.5999999999987279953, 1.000000000000000000),
 ( 0.2500000000000000000, 0.2499999999993640087, 0.2999999999990460298, 0.3999999999987279842, 0.5999999999987279953, 1.000000000000000000),
 ( 0.2500000000000000000, 0.2499999999993640087, 0.2999999999990460298, 0.3999999999987279842, 0.5999999999987279953, 1.000000000000000000),
 ( 0.2500000000000000000, 0.2499999999993640087, 0.2999999999990460298, 0.3999999999987279842, 0.5999999999987279953, 1.000000000000000000),
 ( 0.2500000000000000000, 0.2499999999993640087, 0.2999999999990460298, 0.3999999999987279842, 0.5999999999987279953, 1.000000000000000000),
 ( 0.2500000000000000000, 0.2499999999993640087, 0.2999999999990460298, 0.3999999999987279842, 0.5999999999987279953, 1.000000000000000000),
 ( 0.2500000000000000000, 0.2499999999993640087, 0.2999999999990460298, 0.3999999999987279842, 0.5999999999987279953, 1.000000000000000000),
 ( 0.2500000000000000000, 0.2499999999993640087, 0.2999999999990460298, 0.3999999999987279842, 0.5999999999987279953, 1.000000000000000000),
 ( 0.2500000000000000000, 0.2499999999993640087, 0.2999999999990460298, 0.3999999999987279842, 0.5999999999987279953, 1.000000000000000000),
 ( 0.2500000000000000000, 0.2499999999993640087, 0.2999999999990460298, 0.3999999999987279842, 0.5999999999987279953, 1.000000000000000000),
 ( 0.2500000000000000000, 0.2499999999993640087, 0.2999999999990460298, 0.3999999999987279842, 0.5999999999987279953, 1.000000000000000000),
 ( 0.2500000000000000000, 0.2499999999993640087, 0.2999999999990460298, 0.3999999999987279842, 0.5999999999987279953, 1.000000000000000000),
 ( 0.2500000000000000000, 0.2499999999993640087, 0.2999999999990460298, 0.3999999999987279842, 0.5999999999987279953, 1.000000000000000000),
 ( 0.2500000000000000000, 0.2499999999993640087, 0.2999999999990460298, 0.3999999999987279842, 0.5999999999987279953, 1.000000000000000000),
 ( 0.2500000000000000000, 0.2499999999993640087, 0.2999999999990460298, 0.3999999999987279842, 0.5999999999987279953, 1.000000000000000000),
 ( 0.2500000000000000000, 0.2499999999993640087, 0.2999999999990460298, 0.3999999999987279842, 0.5999999999987279953, 1.000000000000000000),
 ( 0.2500000000000000000, 0.2499999999993640087, 0.2999999999990460298, 0.3999999999987279842, 0.5999999999987279953, 1.000000000000000000),
 ( 0.2500000000000000000, 0.2499999999993640087, 0.2999999999990460298, 0.3999999999987279842, 0.5999999999987279953, 1.000000000000000000),
 ( 0.2500000000000000000, 0.2499999999993640087, 0.2999999999990460298, 0.3999999999987279842, 0.5999999999987279953, 1.000000000000000000),
 ( 0.2500000000000000000, 0.2499999999993640087, 0.2999999999990460298, 0.3999999999987279842, 0.5999999999987279953, 1.000000000000000000),
 ( 0.2500000000000000000, 0.2499999999993640087, 0.2999999999990460298, 0.3999999999987279842, 0.5999999999987279953, 1.000000000000000000),
 ( 0.2500000000000000000, 0.2499999999993640087, 0.2999999999990460298, 0.3999999999987279842, 0.5999999999987279953, 1.000000000000000000),
 ( 0.2500000000000000000, 0.2499999999993640087, 0.2999999999990460298, 0.3999999999987279842, 0.5999999999987279953, 1.000000000000000000),
 ( 0.2500000000000000000, 0.2499999999993640087, 0.2999999999990460298, 0.3999999999987279842, 0.5999999999987279953, 1.000000000000000000),
 ( 0.2500000000000000000, 0.2499999999993640087, 0.2999999999990460298, 0.3999999999987279842, 0.5999999999987279953, 1.000000000000000000),
 ( 0.2500000000000000000, 0.2499999999993640087, 0.2999999999990460298, 0.3999999999987279842, 0.5999999999987279953, 1.000000000000000000),
 ( 0.2500000000000000000, 0.2499999999993640087, 0.2999999999990460298, 0.3999999999987279842, 0.5999999999987279953, 1.000000000000000000),
 ( 0.2500000000000000000, 0.2499999999993640087, 0.2999999999990460298, 0.3999999999987279842, 0.5999999999987279953, 1.000000000000000000),
 ( 0.2500000000000000000, 0.2499999999993640087, 0.2999999999990460298, 0.3999999999987279842, 0.5999999999987279953, 1.000000000000000000),
 ( 0.2500000000000000000, 0.2499999999993640087, 0.2999999999990460298, 0.3999999999987279842, 0.5999999999987279953, 1.000000000000000000),
 ( 0.2500000000000000000, 0.2499999999993640087, 0.2999999999990460298, 0.3999999999987279842, 0.5999999999987279953, 1.000000000000000000),
 ( 0.2500000000000000000, 0.2499999999993640087, 0.2999999999990460298, 0.3999999999987279842, 0.5999999999987279953, 1.000000000000000000),
 ( 0.2500000000000000000, 0.2499999999993640087, 0.2999999999990460298, 0.3999999999987279842, 0.5999999999987279953, 1.000000000000000000),
 ( 0.2500000000000000000, 0.2499999999993640087, 0.2999999999990460298, 0.3999999999987279842, 0.5999999999987279953, 1.000000000000000000),
 ( 0.2500000000000000000, 0.2499999999993640087, 0.2999999999990460298, 0.3999999999987279842, 0.5999999999987279953, 1.000000000000000000),
 ( 0.2500000000000000000, 0.2499999999993640087, 0.2999999999990460298, 0.3999999999987279842, 0.5999999999987279953, 1.000000000000000000),
 ( 0.2500000000000000000, 0.2499999999993640087, 0.2999999999990460298, 0.3999999999987279842, 0.5999999999987279953, 1.000000000000000000),
 ( 0.2500000000000000000, 0.2499999999993640087, 0.2999999999990460298, 0.3999999999987279842, 0.5999999999987279953, 1.000000000000000000),
 ( 0.2500000000000000000, 0.2499999999993640087, 0.2999999999990460298, 0.3999999999987279842, 0.5999999999987279953, 1.000000000000000000),
 ( 0.2500000000000000000, 0.2499999999993640087, 0.2999999999990460298, 0.3999999999987279842, 0.5999999999987279953, 1.000000000000000000),
 ( 0.2500000000000000000, 0.2499999999993640087, 0.2999999999990460298, 0.3999999999987279842, 0.5999999999987279953, 1.000000000000000000),
 ( 0.2500000000000000000, 0.2499999999993640087, 0.2999999999990460298, 0.3999999999987279842, 0.5999999999987279953, 1.000000000000000000),
 ( 0.2500000000000000000, 0.2499999999993640087, 0.2999999999990460298, 0.3999999999987279842, 0.5999999999987279953, 1.000000000000000000),
 ( 0.2500000000000000000, 0.2499999999993640087, 0.2999999999990460298, 0.3999999999987279842, 0.5999999999987279953, 1.000000000000000000),
 ( 0.2500000000000000000, 0.2499999999993640087, 0.2999999999990460298, 0.3999999999987279842, 0.5999999999987279953, 1.000000000000000000),
 ( 0.2500000000000000000, 0.2499999999993640087, 0.2999999999990460298, 0.3999999999987279842, 0.5999999999987279953, 1.000000000000000000),
 ( 0.2500000000000000000, 0.2499999999993640087, 0.2999999999990460298, 0.3999999999987279842, 0.5999999999987279953, 1.000000000000000000) ) ) 
 REPRESENTATION_ITEM ( '' )  SURFACE ( )  );
#21494=CARTESIAN_POINT ( 'NONE',  ( 5.679423221865293137, 1366.539118458927078, 209.6218459617148824 ) ) ;
#21522=CARTESIAN_POINT ( 'NONE',  ( 7.818221670759999853, 1367.736483592530021, 207.6218459616989946 ) ) ;
#21632=AXIS2_PLACEMENT_3D ( 'NONE', #110085, #42890, #42328 ) ;
#21633=CARTESIAN_POINT ( 'NONE',  ( 4.262353028419999745, 1360.811275533920025, 207.6218459616989946 ) ) ;
#21648=CARTESIAN_POINT ( 'NONE',  ( 7.622608667027140683, 1359.902596381179819, 208.3718459617010978 ) ) ;
#21671=CARTESIAN_POINT ( 'NONE',  ( -9.516636888345459511, 1366.309137899877896, 210.6218459616987957 ) ) ;
#21677=LINE ( 'NONE', #22773, #82980 ) ;
#21766=CARTESIAN_POINT ( 'NONE',  ( -11.55751048842087059, 1366.520570492055640, 208.3718459617010978 ) ) ;
#21904=CARTESIAN_POINT ( 'NONE',  ( 9.663424421700000266, 1363.752474719050042, 210.6218459616991936 ) ) ;
#21987=ORIENTED_EDGE ( 'NONE', *, *, #17933, .F. ) ;
#22038=CARTESIAN_POINT ( 'NONE',  ( 7.862230021551401826, 1365.371610286726764, 208.3718459617061285 ) ) ;
#22065=CARTESIAN_POINT ( 'NONE',  ( 9.532517564019999057, 1366.286862064870093, 207.6218459616989946 ) ) ;
#22080=CARTESIAN_POINT ( 'NONE',  ( -9.572080927779999334E-17, 1389.913060387289988, 209.1218459616989946 ) ) ;
#22176=CARTESIAN_POINT ( 'NONE',  ( -0.7618909056700008398, 1360.403425203260213, 207.6218459616989946 ) ) ;
#22193=CARTESIAN_POINT ( 'NONE',  ( 9.704582620014180705, 1366.001145740636048, 210.6218459616991936 ) ) ;
#22218=CARTESIAN_POINT ( 'NONE',  ( -8.589335072474291621, 1365.868898122805376, 207.6218459616988241 ) ) ;
#22236=CARTESIAN_POINT ( 'NONE',  ( -3.061616997868380553E-17, 1389.413060387289988, 209.1218459616989946 ) ) ;
#22317=CARTESIAN_POINT ( 'NONE',  ( -10.61207710156363149, 1361.707344756497832, 209.6218459617033432 ) ) ;
#22370=DIRECTION ( 'NONE',  ( -6.123233995736769734E-17, -1.000000000000000000, -1.124819836996399911E-32 ) ) ;
#22448=DIRECTION ( 'NONE',  ( 0.9900965937346508650, -0.1403878024439509931, 3.790652827686682019E-16 ) ) ;
#22455=CARTESIAN_POINT ( 'NONE',  ( 9.971295257850000482, 1364.502667329740007, 210.6218459616991936 ) ) ;
#22462=ORIENTED_EDGE ( 'NONE', *, *, #29916, .F. ) ;
#22585=CARTESIAN_POINT ( 'NONE',  ( 7.917631394359482044, 1366.221626954849626, 210.6218459617142003 ) ) ;
#22652=ORIENTED_EDGE ( 'NONE', *, *, #104492, .F. ) ;
#22656=CARTESIAN_POINT ( 'NONE',  ( -3.464457313471830169, 1370.273648968840689, 210.1175475933252130 ) ) ;
#22724=CARTESIAN_POINT ( 'NONE',  ( 0.05351389538980268201, 1362.267411265992223, 208.3718459617061285 ) ) ;
#22741=CARTESIAN_POINT ( 'NONE',  ( 9.532517564019499900, 1366.286862064863953, 210.6218459616991936 ) ) ;
#22766=CARTESIAN_POINT ( 'NONE',  ( -8.059092760027739999, 1365.100440301198660, 208.3718459617061285 ) ) ;
#22773=CARTESIAN_POINT ( 'NONE',  ( -2.632747685671116500, 1379.913060387289988, 207.6835693458863830 ) ) ;
#22872=CARTESIAN_POINT ( 'NONE',  ( -9.655745333040000489, 1363.739547551590022, 207.6218459616989946 ) ) ;
#23020=CARTESIAN_POINT ( 'NONE',  ( 6.358435812109999752, 1368.427897723179967, 210.6218459616991936 ) ) ;
#23255=DIRECTION ( 'NONE',  ( -6.123233995736769734E-17, -1.000000000000000000, -1.124819836996399911E-32 ) ) ;
#23293=CARTESIAN_POINT ( 'NONE',  ( 9.663424421720160140, 1363.752474719036172, 210.6218459616987957 ) ) ;
#23305=EDGE_CURVE ( 'NONE', #33810, #76110, #86513, .T. ) ;
#23313=CARTESIAN_POINT ( 'NONE',  ( 12.04322937582876030, 1364.845882714125537, 209.6218459617033432 ) ) ;
#23443=CARTESIAN_POINT ( 'NONE',  ( -9.655745333031781286, 1363.739547551595933, 210.6218459616991936 ) ) ;
#23578=CARTESIAN_POINT ( 'NONE',  ( -3.763781937370000108, 1369.097489338550076, 207.6218459616989946 ) ) ;
#23584=ORIENTED_EDGE ( 'NONE', *, *, #19347, .F. ) ;
#23613=B_SPLINE_CURVE_WITH_KNOTS ( 'NONE', 3,
 ( #95832, #87444, #10739, #54415, #88547, #98023, #63373, #11832, #80134, #12369, #46555, #72308, #70126, #21295, #78489, #1803, #44912, #36477, #48200, #6174, #48756, #31372 ),
 .UNSPECIFIED., .F., .F.,
 ( 4, 2, 2, 2, 2, 2, 2, 2, 2, 2, 4 ),
 ( 0.000000000000000000, 0.0004646859671260076966, 0.0009293719342520153932, 0.001394057901378022981, 0.001626400884941100501, 0.001858743868504178238, 0.002091086852067255974, 0.002323429835630333711, 0.002788115802756573319, 0.003252801769882813360, 0.003717487737009052967 ),
 .UNSPECIFIED. ) ;
#23634=VERTEX_POINT ( 'NONE', #78875 ) ;
#23727=DIRECTION ( 'NONE',  ( 3.828568698926946970E-16, 0.000000000000000000, -1.000000000000000000 ) ) ;
#23838=CARTESIAN_POINT ( 'NONE',  ( 9.813910351429941059, 1364.017814053639768, 210.6218459616987957 ) ) ;
#23855=CARTESIAN_POINT ( 'NONE',  ( 10.57963509885960285, 1366.486042548352543, 207.6218459616987673 ) ) ;
#23979=CARTESIAN_POINT ( 'NONE',  ( -9.832966357653941003, 1364.062280235955768, 210.6218459616991936 ) ) ;
#24027=LINE ( 'NONE', #16183, #15530 ) ;
#24173=CYLINDRICAL_SURFACE ( 'NONE', #63860, 9.999999999999992895 ) ;
#24239=FACE_OUTER_BOUND ( 'NONE', #80929, .T. ) ;
#24333=EDGE_CURVE ( 'NONE', #5019, #36878, #56928, .T. ) ;
#24334=CARTESIAN_POINT ( 'NONE',  ( -4.457338102780003197, 1370.468904865611648, 209.2786786533806946 ) ) ;
#24344=ORIENTED_EDGE ( 'NONE', *, *, #10750, .F. ) ;
#24395=CARTESIAN_POINT ( 'NONE',  ( 7.893629640421917948, 1363.336479960825272, 207.6218459616988241 ) ) ;
#24409=CARTESIAN_POINT ( 'NONE',  ( 9.925983360900000108, 1364.303202023270160, 207.6218459616989946 ) ) ;
#24475=DIRECTION ( 'NONE',  ( 0.1403901532130676921, 0.9900962604114871279, 1.240732444514164729E-15 ) ) ;
#24488=AXIS2_PLACEMENT_3D ( 'NONE', #28607, #103087, #62807 ) ;
#24533=CARTESIAN_POINT ( 'NONE',  ( -8.454776581079805453, 1360.296086664740642, 208.3718459617010978 ) ) ;
#24644=CARTESIAN_POINT ( 'NONE',  ( -7.173827098650000345, 1361.757975858899954, 207.6218459616989946 ) ) ;
#24930=CARTESIAN_POINT ( 'NONE',  ( 7.871876822161247844, 1364.664245783809292, 209.6218459617148824 ) ) ;
#24943=SHAPE_REPRESENTATION_RELATIONSHIP ( 'NONE' , 'NONE' ,  #83713, #110798 ) ;
#24945=CARTESIAN_POINT ( 'NONE',  ( 9.663829730717637290, 1367.635736277483147, 207.6218459616987673 ) ) ;
#25086=CARTESIAN_POINT ( 'NONE',  ( -0.8025614321512887228, 1359.202926620322387, 210.6218459617030021 ) ) ;
#25206=CARTESIAN_POINT ( 'NONE',  ( -7.891625280017878552, 1364.691779921422949, 209.6218459617148824 ) ) ;
#25231=CIRCLE ( 'NONE', #73562, 2.000000000000003553 ) ;
#25239=DIRECTION ( 'NONE',  ( -1.000000000000000000, 6.123233995736769734E-17, 0.000000000000000000 ) ) ;
#25390=PRODUCT_DEFINITION ( 'UNKNOWN', '', #69102, #60314 ) ;
#25492=CARTESIAN_POINT ( 'NONE',  ( 8.159621828281631295, 1363.533245305855644, 207.6218459616988241 ) ) ;
#25506=CARTESIAN_POINT ( 'NONE',  ( 4.938621453790089433, 1370.910692062234148, 209.6218459617033432 ) ) ;
#25642=CARTESIAN_POINT ( 'NONE',  ( 6.171356481870118316, 1359.214203302260557, 209.6218459617033432 ) ) ;
#25763=CARTESIAN_POINT ( 'NONE',  ( -7.592250591143125504, 1364.366890427691942, 209.6218459617148824 ) ) ;
#25771=CARTESIAN_POINT ( 'NONE',  ( -9.209502321770001387, 1366.683160837839978, 207.6218459616989946 ) ) ;
#25781=VERTEX_POINT ( 'NONE', #52922 ) ;
#26039=CARTESIAN_POINT ( 'NONE',  ( 8.963248341601568470, 1364.599977456154647, 207.6218459616988241 ) ) ;
#26054=CARTESIAN_POINT ( 'NONE',  ( 8.795499755375784545, 1368.316259268678550, 207.6218459616987673 ) ) ;
#26122=CARTESIAN_POINT ( 'NONE',  ( -8.775825618903718706, 1379.913060387289988, 204.3275905756569841 ) ) ;
#26196=CARTESIAN_POINT ( 'NONE',  ( -0.8254386033013292323, 1358.527646167416151, 208.3718459617010978 ) ) ;
#26223=CARTESIAN_POINT ( 'NONE',  ( -3.585211238355716645, 1368.112806773307057, 207.6218459616988241 ) ) ;
#26318=CARTESIAN_POINT ( 'NONE',  ( -9.328535443866920573, 1363.278783432113869, 210.6218459616987957 ) ) ;
#26327=CARTESIAN_POINT ( 'NONE',  ( -6.371134682390000137, 1368.423166410909971, 207.6218459616989946 ) ) ;
#26383=CARTESIAN_POINT ( 'NONE',  ( -2.887288154357296133, 1368.159587626394341, 207.9537811227674808 ) ) ;
#26535=AXIS2_PLACEMENT_3D ( 'NONE', #28097, #18569, #52764 ) ;
#26606=CARTESIAN_POINT ( 'NONE',  ( 9.971295257839999593, 1364.502667329740007, 207.6218459616989946 ) ) ;
#26621=FILL_AREA_STYLE_COLOUR ( '', #35973 ) ;
#26623=CARTESIAN_POINT ( 'NONE',  ( 7.445922712490000706, 1367.935115748530052, 207.6218459616989946 ) ) ;
#26633=CARTESIAN_POINT ( 'NONE',  ( -0.7618909056700008398, 1360.403425203260213, 207.6218459616989946 ) ) ;
#26761=CARTESIAN_POINT ( 'NONE',  ( 4.262353028419999745, 1360.811275533920025, 207.6218459616989946 ) ) ;
#26788=CARTESIAN_POINT ( 'NONE',  ( -8.436812995028324380, 1365.738857087742417, 210.6218459617142003 ) ) ;
#26809=AXIS2_PLACEMENT_3D ( 'NONE', #34881, #50048, #103170 ) ;
#26873=CARTESIAN_POINT ( 'NONE',  ( -2.829895884882737356, 1367.754820046488248, 209.5158523731048206 ) ) ;
#26891=CARTESIAN_POINT ( 'NONE',  ( -8.626596292616463657, 1364.357876662198805, 210.6218459617142003 ) ) ;
#26900=CARTESIAN_POINT ( 'NONE',  ( -9.841049031033593408, 1368.780040876450585, 209.6218459617033432 ) ) ;
#26961=DIRECTION ( 'NONE',  ( 6.123233995736769734E-17, 1.000000000000000000, 1.124819836996399911E-32 ) ) ;
#27140=EDGE_CURVE ( 'NONE', #68445, #96281, #89702, .T. ) ;
#27176=CARTESIAN_POINT ( 'NONE',  ( 7.990250629489356271, 1364.963476878560641, 209.6218459617148824 ) ) ;
#27190=CARTESIAN_POINT ( 'NONE',  ( 10.29084807479042318, 1367.270713213549698, 210.6218459617030021 ) ) ;
#27201=CARTESIAN_POINT ( 'NONE',  ( -9.934709065799999905, 1365.494406819939968, 207.6218459616989946 ) ) ;
#27208=CIRCLE ( 'NONE', #64727, 10.00000000000000888 ) ;
#27315=CARTESIAN_POINT ( 'NONE',  ( -0.7618909056619500575, 1360.403425203269990, 210.6218459616991936 ) ) ;
#27338=CARTESIAN_POINT ( 'NONE',  ( -8.624710350820000926, 1367.191948709370081, 207.6218459616989946 ) ) ;
#27430=CARTESIAN_POINT ( 'NONE',  ( 6.113148423521039376, 1363.477843159564372, 209.6218459617148824 ) ) ;
#27439=CARTESIAN_POINT ( 'NONE',  ( -7.450033292398919649, 1367.931913175455975, 210.6218459616991936 ) ) ;
#27477=SURFACE_STYLE_FILL_AREA ( #95244 ) ;
#27620=EDGE_LOOP ( 'NONE', ( #16771, #28720, #73115, #58450 ) ) ;
#27723=CARTESIAN_POINT ( 'NONE',  ( 7.901460997567876454, 1365.119847262537405, 209.6218459617148824 ) ) ;
#27745=CARTESIAN_POINT ( 'NONE',  ( 9.622136349630000751, 1363.684386430210225, 207.6218459616989946 ) ) ;
#27860=VERTEX_POINT ( 'NONE', #5733 ) ;
#27874=CARTESIAN_POINT ( 'NONE',  ( 9.454737631248359975, 1363.431170718790099, 210.6218459616991936 ) ) ;
#27898=CARTESIAN_POINT ( 'NONE',  ( -6.030651517141524920, 1367.479084863156004, 207.6218459616988241 ) ) ;
#27989=CARTESIAN_POINT ( 'NONE',  ( -5.986709854369999917, 1361.264879806939916, 207.6218459616989946 ) ) ;
#27997=CARTESIAN_POINT ( 'NONE',  ( -9.248485401361245195, 1369.066561549477910, 208.3718459617010978 ) ) ;
#28097=CARTESIAN_POINT ( 'NONE',  ( -1.122592899216370017E-16, 1388.079727053959914, 209.1218459616989946 ) ) ;
#28124=EDGE_CURVE ( 'NONE', #92455, #27860, #109966, .T. ) ;
#28200=TOROIDAL_SURFACE ( 'NONE', #15602, 3.500000000000000000, 0.5000000000000000000 ) ;
#28274=CARTESIAN_POINT ( 'NONE',  ( 9.369782510150898247, 1366.497526915296021, 210.6218459616987957 ) ) ;
#28301=CARTESIAN_POINT ( 'NONE',  ( 9.984115569220000097, 1365.258395869459946, 207.6218459616989946 ) ) ;
#28426=CARTESIAN_POINT ( 'NONE',  ( 9.570655340201339456, 1361.000351557653630, 208.3718459617010978 ) ) ;
#28444=CIRCLE ( 'NONE', #37397, 9.500000000000008882 ) ;
#28452=CARTESIAN_POINT ( 'NONE',  ( -8.158278992428673604, 1366.026982084109250, 210.6218459617142003 ) ) ;
#28459=CIRCLE ( 'NONE', #1700, 0.4999999999999976130 ) ;
#28552=CARTESIAN_POINT ( 'NONE',  ( -11.86834588888874187, 1366.062423491164964, 209.6218459617033432 ) ) ;
#28607=CARTESIAN_POINT ( 'NONE',  ( -8.337034337958545649, 1374.413060387289988, 204.5673033449591003 ) ) ;
#28677=CARTESIAN_POINT ( 'NONE',  ( 1.050222213330426424, 1370.064815538551329, 206.9592408025515624 ) ) ;
#28696=CARTESIAN_POINT ( 'NONE',  ( -8.624710350819999150, 1367.191948709370081, 210.6218459616991936 ) ) ;
#28720=ORIENTED_EDGE ( 'NONE', *, *, #8381, .T. ) ;
#28769=EDGE_CURVE ( 'NONE', #88920, #76110, #74605, .T. ) ;
#28833=CARTESIAN_POINT ( 'NONE',  ( 6.358435812139999754, 1368.427897723179740, 207.6218459616989946 ) ) ;
#28849=CARTESIAN_POINT ( 'NONE',  ( 3.005276066430000448, 1369.205039411269809, 207.6218459616989946 ) ) ;
#28860=CARTESIAN_POINT ( 'NONE',  ( 9.842969107809999230, 1365.740588703660023, 207.6218459616989946 ) ) ;
#28984=CARTESIAN_POINT ( 'NONE',  ( 10.40058593205784909, 1361.671709241824374, 208.3718459617010978 ) ) ;
#29009=CARTESIAN_POINT ( 'NONE',  ( -8.075791892808387828, 1366.351623811200170, 207.6218459616988241 ) ) ;
#29064=EDGE_CURVE ( 'NONE', #60506, #74686, #107669, .T. ) ;
#29084=CARTESIAN_POINT ( 'NONE',  ( -2.980426153849875082, 1368.816447224659214, 210.5740313466029647 ) ) ;
#29103=CARTESIAN_POINT ( 'NONE',  ( -11.74749358745221173, 1366.026922449215363, 208.3718459617010978 ) ) ;
#29228=DIRECTION ( 'NONE',  ( -0.8775825618903763115, 0.000000000000000000, -0.4794255386041965106 ) ) ;
#29230=CARTESIAN_POINT ( 'NONE',  ( 3.099041906601330165, 1369.866330758129379, 210.4936753499222561 ) ) ;
#29237=CARTESIAN_POINT ( 'NONE',  ( 2.880867337579580134, 1368.384084939549894, 207.8228488383560091 ) ) ;
#29364=CARTESIAN_POINT ( 'NONE',  ( 5.951028257965643498, 1367.294630164640239, 210.6218459617142003 ) ) ;
#29389=CARTESIAN_POINT ( 'NONE',  ( 3.005276066430000448, 1369.205039411269809, 207.6218459616989946 ) ) ;
#29519=CARTESIAN_POINT ( 'NONE',  ( 9.515060695661910373, 1360.808172452092322, 209.6218459617033432 ) ) ;
#29543=CARTESIAN_POINT ( 'NONE',  ( -9.977700672470000143, 1365.292605733890014, 207.6218459616989946 ) ) ;
#29642=CARTESIAN_POINT ( 'NONE',  ( -11.56214142042087367, 1363.316088303152810, 208.3718459617010978 ) ) ;
#29748=CARTESIAN_POINT ( 'NONE',  ( -2.919110404717550011, 1368.384062535930070, 207.8228080779019820 ) ) ;
#29766=ORIENTED_EDGE ( 'NONE', *, *, #93229, .T. ) ;
#29786=CARTESIAN_POINT ( 'NONE',  ( 9.454737631250001328, 1363.431170718790099, 210.6218459616991936 ) ) ;
#29866=AXIS2_PLACEMENT_3D ( 'NONE', #19075, #53279, #36448 ) ;
#29911=CARTESIAN_POINT ( 'NONE',  ( 7.818221670743039198, 1367.736483592547984, 210.6218459616987957 ) ) ;
#29916=EDGE_CURVE ( 'NONE', #33810, #77151, #55513, .T. ) ;
#30046=CARTESIAN_POINT ( 'NONE',  ( -0.7618909056627740650, 1360.403425203244069, 210.6218459616987957 ) ) ;
#30062=CARTESIAN_POINT ( 'NONE',  ( 10.48770262178695667, 1361.581614096479370, 209.6218459617033432 ) ) ;
#30084=CARTESIAN_POINT ( 'NONE',  ( -9.690020260109999839, 1366.026910387849966, 207.6218459616989946 ) ) ;
#30091=DIRECTION ( 'NONE',  ( -6.123233995736769734E-17, -1.000000000000000000, 0.000000000000000000 ) ) ;
#30183=CARTESIAN_POINT ( 'NONE',  ( -10.11455584700109966, 1367.169308473507954, 207.6218459616987673 ) ) ;
#30184=CARTESIAN_POINT ( 'NONE',  ( -5.843535329920999999, 1389.008761609309886, 209.1218459616989946 ) ) ;
#30332=CARTESIAN_POINT ( 'NONE',  ( 5.215187551930000609, 1368.779556716640172, 210.6218459616991936 ) ) ;
#30471=CARTESIAN_POINT ( 'NONE',  ( 8.726849315049999944, 1367.111769039820047, 207.6218459616989946 ) ) ;
#30610=CARTESIAN_POINT ( 'NONE',  ( 1.748848150597736018, 1360.440694539904143, 210.6218459616987957 ) ) ;
#30627=CARTESIAN_POINT ( 'NONE',  ( 11.94297283982292335, 1364.098416124965070, 209.6218459617033432 ) ) ;
#30650=CARTESIAN_POINT ( 'NONE',  ( -9.830395177452579958, 1365.769828494191870, 210.6218459616987957 ) ) ;
#30745=CARTESIAN_POINT ( 'NONE',  ( -11.95567671777125085, 1365.667439879733138, 209.6218459617033432 ) ) ;
#30786=ORIENTED_EDGE ( 'NONE', *, *, #53835, .T. ) ;
#30874=FACE_OUTER_BOUND ( 'NONE', #93611, .T. ) ;
#31019=CARTESIAN_POINT ( 'NONE',  ( 7.331153383319085393, 1366.861207034019344, 207.6218459616988241 ) ) ;
#31150=CARTESIAN_POINT ( 'NONE',  ( 1.602682243905599213, 1362.313628982924683, 208.3718459617061285 ) ) ;
#31165=CARTESIAN_POINT ( 'NONE',  ( 9.671060821790000261, 1366.060403940050037, 207.6218459616989946 ) ) ;
#31193=CARTESIAN_POINT ( 'NONE',  ( -8.121968579123178600, 1364.865207952712808, 208.3718459617061285 ) ) ;
#31296=CARTESIAN_POINT ( 'NONE',  ( -9.569455633217616608, 1362.104322562968264, 207.6218459616987673 ) ) ;
#31372=CARTESIAN_POINT ( 'NONE',  ( 3.149414619133680482, 1370.221588481574372, 210.2153961732977905 ) ) ;
#31428=DIRECTION ( 'NONE',  ( 0.8775825618903727587, 9.629649721936177897E-33, 0.4794255386042027833 ) ) ;
#31431=CARTESIAN_POINT ( 'NONE',  ( -3.145663868875199221, 1370.195136005008180, 207.6218459616987673 ) ) ;
#31466=CARTESIAN_POINT ( 'NONE',  ( -2.836810703500213027, 1368.016923498806364, 210.6218459617142003 ) ) ;
#31663=CARTESIAN_POINT ( 'NONE',  ( 7.889195814119081440, 1372.293237941190000, 213.4317332778174716 ) ) ;
#31702=CARTESIAN_POINT ( 'NONE',  ( 8.396902068309636036, 1363.743897584764454, 207.6218459616988241 ) ) ;
#31717=CARTESIAN_POINT ( 'NONE',  ( 11.34530601785825965, 1366.910327255101038, 208.3718459617010978 ) ) ;
#31742=CARTESIAN_POINT ( 'NONE',  ( -8.001072242696793069, 1364.926390148715655, 209.6218459617148824 ) ) ;
#31849=CARTESIAN_POINT ( 'NONE',  ( -10.22852398056611278, 1361.350133274729160, 209.6218459617033432 ) ) ;
#31958=B_SPLINE_CURVE_WITH_KNOTS ( 'NONE', 3,
 ( #107561, #3481, #63936, #99141 ),
 .UNSPECIFIED., .F., .F.,
 ( 4, 4 ),
 ( 0.000000000000000000, 1.000000000000000000 ),
 .UNSPECIFIED. ) ;
#31986=CARTESIAN_POINT ( 'NONE',  ( -3.173741429363529321, 1370.393155323753945, 210.6218459617030021 ) ) ;
#31988=CARTESIAN_POINT ( 'NONE',  ( 8.796059898599999372, 1362.759824263850078, 210.6218459616991936 ) ) ;
#32022=CARTESIAN_POINT ( 'NONE',  ( -3.428961876718509050, 1367.251209528720665, 208.3718459617061285 ) ) ;
#32037=VERTEX_POINT ( 'NONE', #12216 ) ;
#32114=EDGE_LOOP ( 'NONE', ( #78237, #79145 ) ) ;
#32150=ORIENTED_EDGE ( 'NONE', *, *, #4208, .T. ) ;
#32169=DIRECTION ( 'NONE',  ( -6.123233995736769734E-17, -1.000000000000000000, -1.124819836996399911E-32 ) ) ;
#32197=CARTESIAN_POINT ( 'NONE',  ( -3.870244853708171284, 1370.348070663988892, 209.9344813661604974 ) ) ;
#32263=CARTESIAN_POINT ( 'NONE',  ( 9.454737631249999552, 1363.431170718789872, 207.6218459616989946 ) ) ;
#32280=CARTESIAN_POINT ( 'NONE',  ( 11.88647226875623986, 1365.999781939073273, 209.6218459617033432 ) ) ;
#32412=CARTESIAN_POINT ( 'NONE',  ( -9.725849732204427056, 1360.959007460116936, 209.6218459617033432 ) ) ;
#32480=DIRECTION ( 'NONE',  ( 0.1403901532130676921, 0.9900962604114871279, 1.240732444514164729E-15 ) ) ;
#32546=CARTESIAN_POINT ( 'NONE',  ( -3.286051671319225598, 1371.185232598742687, 209.6218459617033432 ) ) ;
#32551=VERTEX_POINT ( 'NONE', #73110 ) ;
#32594=ORIENTED_EDGE ( 'NONE', *, *, #110303, .T. ) ;
#32801=CARTESIAN_POINT ( 'NONE',  ( 6.474683829332638751, 1363.643362496321288, 209.6218459617148824 ) ) ;
#32816=CARTESIAN_POINT ( 'NONE',  ( 11.57989268124586424, 1366.469131039695867, 208.3718459617010978 ) ) ;
#32823=ORIENTED_EDGE ( 'NONE', *, *, #44729, .T. ) ;
#32945=CARTESIAN_POINT ( 'NONE',  ( -8.538839991155660059, 1362.569232148552146, 210.6218459616991936 ) ) ;
#32970=ORIENTED_EDGE ( 'NONE', *, *, #10750, .T. ) ;
#33005=CARTESIAN_POINT ( 'NONE',  ( 3.125365561257785973, 1370.051980510865860, 207.8674606832949507 ) ) ;
#33112=EDGE_LOOP ( 'NONE', ( #82988, #50281, #919, #36990 ) ) ;
#33331=ORIENTED_EDGE ( 'NONE', *, *, #29064, .F. ) ;
#33346=CARTESIAN_POINT ( 'NONE',  ( 6.528782948190136715, 1363.530450965401315, 208.3718459617061285 ) ) ;
#33362=CARTESIAN_POINT ( 'NONE',  ( 6.358435812109480167, 1368.427897723174055, 210.6218459616991936 ) ) ;
#33425=DIRECTION ( 'NONE',  ( 1.192122195693504081E-14, -4.372198439846870180E-16, -1.000000000000000000 ) ) ;
#33466=CARTESIAN_POINT ( 'NONE',  ( 2.880836473691240407, 1368.383867273139913, 210.4211859087380105 ) ) ;
#33486=CARTESIAN_POINT ( 'NONE',  ( -6.297634499852111212, 1360.310814921950850, 207.6218459616987673 ) ) ;
#33606=ORIENTED_EDGE ( 'NONE', *, *, #93229, .F. ) ;
#33609=CARTESIAN_POINT ( 'NONE',  ( -7.426018358933801800, 1364.078817793960070, 208.3718459617061285 ) ) ;
#33664=ADVANCED_FACE ( 'NONE', ( #11445 ), #84289, .F. ) ;
#33810=VERTEX_POINT ( 'NONE', #109088 ) ;
#33825=DIRECTION ( 'NONE',  ( 3.828568698926946970E-16, 0.000000000000000000, -1.000000000000000000 ) ) ;
#33903=CARTESIAN_POINT ( 'NONE',  ( 7.697803989957441750, 1363.443082852748375, 210.6218459617142003 ) ) ;
#33919=CARTESIAN_POINT ( 'NONE',  ( 4.720156707528646578, 1369.933505578754648, 207.6218459616987673 ) ) ;
#34015=( BOUNDED_SURFACE ( )  B_SPLINE_SURFACE ( 5, 5, ( 
 ( #108694, #31431, #99725, #32546, #31986, #66176 ),
 ( #23578, #66720, #83480, #70041, #53221, #52662 ),
 ( #16801, #61089, #68930, #19018, #51004, #10090 ),
 ( #103600, #36396, #87360, #17917, #60519, #94085 ),
 ( #26327, #70585, #59, #94642, #95204, #62182 ),
 ( #44825, #10656, #2282, #43156, #104702, #27439 ),
 ( #85136, #44264, #8422, #78978, #52113, #1164 ),
 ( #77312, #51551, #27997, #35857, #34190, #78406 ),
 ( #8984, #86243, #18465, #26900, #86799, #104153 ),
 ( #9534, #42593, #76747, #61622, #1718, #95754 ),
 ( #17355, #43702, #77855, #68374, #102482, #103030 ),
 ( #25771, #59970, #85687, #610, #35294, #34740 ),
 ( #69479, #30183, #4461, #54332, #36941, #47562 ),
 ( #106896, #38055, #4990, #80053, #38589, #39135 ),
 ( #80610, #81684, #11215, #3374, #3925, #106356 ),
 ( #73313, #87928, #98498, #88462, #64375, #2822 ),
 ( #81146, #105825, #21766, #90090, #72232, #45379 ),
 ( #71707, #54873, #29103, #28552, #55967, #88996 ),
 ( #13374, #107449, #63829, #30745, #96308, #62751 ),
 ( #63289, #53791, #71138, #97403, #55418, #37501 ),
 ( #96869, #19587, #47021, #12284, #79518, #46478 ),
 ( #11748, #21209, #97941, #89552, #20673, #20138 ),
 ( #105258, #45917, #29642, #12841, #72768, #23979 ),
 ( #14487, #66592, #83351, #49226, #64926, #99589 ),
 ( #22872, #65480, #50339, #100158, #99039, #23443 ),
 ( #40803, #67135, #109669, #48679, #57081, #73871 ),
 ( #83905, #57638, #108559, #90646, #100696, #13929 ),
 ( #92856, #91752, #82802, #22317, #41369, #107999 ),
 ( #40251, #31296, #91205, #31849, #66036, #16132 ),
 ( #74433, #6096, #15027, #6650, #74982, #84464 ),
 ( #56519, #109130, #41916, #32412, #101233, #32945 ),
 ( #58174, #92302, #48116, #15572, #49774, #7211 ),
 ( #75534, #39705, #24533, #58721, #7751, #82255 ),
 ( #76072, #110213, #5556, #52534, #86667, #69906 ),
 ( #69345, #33486, #77726, #85548, #35717, #67688 ),
 ( #61496, #9415, #53090, #104020, #34611, #77185 ),
 ( #85000, #95626, #43577, #44134, #86121, #87229 ),
 ( #9963, #10518, #95077, #17779, #18895, #59290 ),
 ( #51980, #1039, #26196, #44692, #25086, #27315 ),
 ( #78268, #50870, #78839, #18343, #43027, #101796 ),
 ( #35161, #93407, #94505, #8844, #102898, #488 ),
 ( #60384, #59833, #1582, #16672, #8295, #103455 ),
 ( #26761, #60950, #42457, #76616, #68797, #110768 ),
 ( #34058, #68251, #102358, #25642, #93956, #17221 ),
 ( #51417, #36268, #21648, #105136, #37938, #3807 ),
 ( #11626, #45250, #46906, #71015, #45804, #71580 ),
 ( #3253, #46357, #55856, #106233, #89975, #13249 ),
 ( #87799, #79937, #2150, #29519, #70458, #38469 ),
 ( #97276, #105702, #28426, #36825, #72646, #21098 ),
 ( #63710, #98376, #62625, #37380, #72118, #12167 ),
 ( #79386, #4338, #28984, #30062, #106771, #81029 ),
 ( #64253, #80491, #97820, #55300, #89433, #88334 ),
 ( #63172, #2700, #104579, #12725, #47439, #27874 ),
 ( #20549, #62055, #96180, #19455, #96743, #53654 ),
 ( #11083, #54753, #20014, #54209, #88883, #14357 ),
 ( #58047, #82686, #14907, #101113, #74850, #58594 ),
 ( #24409, #56391, #48549, #5976, #49098, #40676 ),
 ( #107331, #75405, #15454, #30627, #90523, #73754 ),
 ( #82122, #109544, #13799, #23313, #73186, #74306 ),
 ( #91631, #47985, #107877, #5424, #6524, #41233 ),
 ( #81563, #39582, #108994, #32280, #100021, #100573 ),
 ( #40121, #108436, #32816, #64815, #91074, #83782 ),
 ( #66464, #23855, #31717, #98923, #65903, #22193 ),
 ( #31165, #57506, #83233, #92725, #65355, #92183 ),
 ( #16001, #99463, #67003, #7077, #4866, #22741 ),
 ( #49646, #39009, #56945, #42330, #27190, #50730 ),
 ( #59156, #102758, #41777, #42892, #35027, #60249 ),
 ( #76482, #24945, #85986, #9828, #8713, #50204 ),
 ( #77595, #43446, #68658, #69206, #103315, #86534 ),
 ( #9284, #84329, #94366, #102227, #52409, #7619 ),
 ( #78132, #26054, #69773, #43997, #51280, #93809 ),
 ( #101658, #1435, #17648, #60819, #51849, #103891 ),
 ( #26623, #61373, #901, #34483, #35581, #75932 ),
 ( #94944, #18213, #77050, #95492, #110087, #33362 ),
 ( #67555, #93276, #16539, #84863, #59696, #8161 ),
 ( #110634, #33919, #356, #25506, #68114, #17088 ),
 ( #85414, #88206, #46772, #55172, #63580, #97150 ),
 ( #28849, #63044, #20419, #54624, #105000, #106102 ) ),
 .UNSPECIFIED., .F., .F., .F. ) 
 B_SPLINE_SURFACE_WITH_KNOTS ( ( 6, 3, 3, 3, 3, 3, 3, 3, 3, 3, 3, 3, 3, 3, 3, 3, 3, 3, 3, 3, 3, 3, 3, 3, 3, 6 ),
 ( 6, 6 ),
 ( 0.000000000000000000, 3.902585213099999617, 6.240861926940000082, 6.790072646649999655, 8.377982366400001268, 8.928580102349998882, 10.97133995140000096, 12.98949692180000071, 13.60228008900000063, 15.24737252870000148, 15.86745694640000082, 18.51059426890000026, 22.57641725190000059, 26.75087197450000076, 31.16005629229999840, 33.90953505430000092, 34.60237748540000524, 36.31249047570000243, 36.97255805550000218, 38.99052022429999909, 41.04947707190000017, 41.62972334150000364, 43.19545136810000230, 43.76106149099999953, 46.17824368760000198, 50.04091111600000374 ),
 ( 0.000000000000000000, 4.712388980389100368 ),
 .UNSPECIFIED. ) 
 GEOMETRIC_REPRESENTATION_ITEM ( )  RATIONAL_B_SPLINE_SURFACE ( (
 ( 1.000000000000000000, 0.5999999999996520339, 0.3999999999996514677, 0.2999999999997390310, 0.2499999999998260003, 0.2500000000000000000),
 ( 1.000000000000000000, 0.5999999999996520339, 0.3999999999996514677, 0.2999999999997390310, 0.2499999999998260003, 0.2500000000000000000),
 ( 1.000000000000000000, 0.5999999999996520339, 0.3999999999996514677, 0.2999999999997390310, 0.2499999999998260003, 0.2500000000000000000),
 ( 1.000000000000000000, 0.5999999999996520339, 0.3999999999996514677, 0.2999999999997390310, 0.2499999999998260003, 0.2500000000000000000),
 ( 1.000000000000000000, 0.5999999999996520339, 0.3999999999996514677, 0.2999999999997390310, 0.2499999999998260003, 0.2500000000000000000),
 ( 1.000000000000000000, 0.5999999999996520339, 0.3999999999996514677, 0.2999999999997390310, 0.2499999999998260003, 0.2500000000000000000),
 ( 1.000000000000000000, 0.5999999999996520339, 0.3999999999996514677, 0.2999999999997390310, 0.2499999999998260003, 0.2500000000000000000),
 ( 1.000000000000000000, 0.5999999999996520339, 0.3999999999996514677, 0.2999999999997390310, 0.2499999999998260003, 0.2500000000000000000),
 ( 1.000000000000000000, 0.5999999999996520339, 0.3999999999996514677, 0.2999999999997390310, 0.2499999999998260003, 0.2500000000000000000),
 ( 1.000000000000000000, 0.5999999999996520339, 0.3999999999996514677, 0.2999999999997390310, 0.2499999999998260003, 0.2500000000000000000),
 ( 1.000000000000000000, 0.5999999999996520339, 0.3999999999996514677, 0.2999999999997390310, 0.2499999999998260003, 0.2500000000000000000),
 ( 1.000000000000000000, 0.5999999999996520339, 0.3999999999996514677, 0.2999999999997390310, 0.2499999999998260003, 0.2500000000000000000),
 ( 1.000000000000000000, 0.5999999999996520339, 0.3999999999996514677, 0.2999999999997390310, 0.2499999999998260003, 0.2500000000000000000),
 ( 1.000000000000000000, 0.5999999999996520339, 0.3999999999996514677, 0.2999999999997390310, 0.2499999999998260003, 0.2500000000000000000),
 ( 1.000000000000000000, 0.5999999999996520339, 0.3999999999996514677, 0.2999999999997390310, 0.2499999999998260003, 0.2500000000000000000),
 ( 1.000000000000000000, 0.5999999999996520339, 0.3999999999996514677, 0.2999999999997390310, 0.2499999999998260003, 0.2500000000000000000),
 ( 1.000000000000000000, 0.5999999999996520339, 0.3999999999996514677, 0.2999999999997390310, 0.2499999999998260003, 0.2500000000000000000),
 ( 1.000000000000000000, 0.5999999999996520339, 0.3999999999996514677, 0.2999999999997390310, 0.2499999999998260003, 0.2500000000000000000),
 ( 1.000000000000000000, 0.5999999999996520339, 0.3999999999996514677, 0.2999999999997390310, 0.2499999999998260003, 0.2500000000000000000),
 ( 1.000000000000000000, 0.5999999999996520339, 0.3999999999996514677, 0.2999999999997390310, 0.2499999999998260003, 0.2500000000000000000),
 ( 1.000000000000000000, 0.5999999999996520339, 0.3999999999996514677, 0.2999999999997390310, 0.2499999999998260003, 0.2500000000000000000),
 ( 1.000000000000000000, 0.5999999999996520339, 0.3999999999996514677, 0.2999999999997390310, 0.2499999999998260003, 0.2500000000000000000),
 ( 1.000000000000000000, 0.5999999999996520339, 0.3999999999996514677, 0.2999999999997390310, 0.2499999999998260003, 0.2500000000000000000),
 ( 1.000000000000000000, 0.5999999999996520339, 0.3999999999996514677, 0.2999999999997390310, 0.2499999999998260003, 0.2500000000000000000),
 ( 1.000000000000000000, 0.5999999999996520339, 0.3999999999996514677, 0.2999999999997390310, 0.2499999999998260003, 0.2500000000000000000),
 ( 1.000000000000000000, 0.5999999999996520339, 0.3999999999996514677, 0.2999999999997390310, 0.2499999999998260003, 0.2500000000000000000),
 ( 1.000000000000000000, 0.5999999999996520339, 0.3999999999996514677, 0.2999999999997390310, 0.2499999999998260003, 0.2500000000000000000),
 ( 1.000000000000000000, 0.5999999999996520339, 0.3999999999996514677, 0.2999999999997390310, 0.2499999999998260003, 0.2500000000000000000),
 ( 1.000000000000000000, 0.5999999999996520339, 0.3999999999996514677, 0.2999999999997390310, 0.2499999999998260003, 0.2500000000000000000),
 ( 1.000000000000000000, 0.5999999999996520339, 0.3999999999996514677, 0.2999999999997390310, 0.2499999999998260003, 0.2500000000000000000),
 ( 1.000000000000000000, 0.5999999999996520339, 0.3999999999996514677, 0.2999999999997390310, 0.2499999999998260003, 0.2500000000000000000),
 ( 1.000000000000000000, 0.5999999999996520339, 0.3999999999996514677, 0.2999999999997390310, 0.2499999999998260003, 0.2500000000000000000),
 ( 1.000000000000000000, 0.5999999999996520339, 0.3999999999996514677, 0.2999999999997390310, 0.2499999999998260003, 0.2500000000000000000),
 ( 1.000000000000000000, 0.5999999999996520339, 0.3999999999996514677, 0.2999999999997390310, 0.2499999999998260003, 0.2500000000000000000),
 ( 1.000000000000000000, 0.5999999999996520339, 0.3999999999996514677, 0.2999999999997390310, 0.2499999999998260003, 0.2500000000000000000),
 ( 1.000000000000000000, 0.5999999999996520339, 0.3999999999996514677, 0.2999999999997390310, 0.2499999999998260003, 0.2500000000000000000),
 ( 1.000000000000000000, 0.5999999999996520339, 0.3999999999996514677, 0.2999999999997390310, 0.2499999999998260003, 0.2500000000000000000),
 ( 1.000000000000000000, 0.5999999999996520339, 0.3999999999996514677, 0.2999999999997390310, 0.2499999999998260003, 0.2500000000000000000),
 ( 1.000000000000000000, 0.5999999999996520339, 0.3999999999996514677, 0.2999999999997390310, 0.2499999999998260003, 0.2500000000000000000),
 ( 1.000000000000000000, 0.5999999999996520339, 0.3999999999996514677, 0.2999999999997390310, 0.2499999999998260003, 0.2500000000000000000),
 ( 1.000000000000000000, 0.5999999999996520339, 0.3999999999996514677, 0.2999999999997390310, 0.2499999999998260003, 0.2500000000000000000),
 ( 1.000000000000000000, 0.5999999999996520339, 0.3999999999996514677, 0.2999999999997390310, 0.2499999999998260003, 0.2500000000000000000),
 ( 1.000000000000000000, 0.5999999999996520339, 0.3999999999996514677, 0.2999999999997390310, 0.2499999999998260003, 0.2500000000000000000),
 ( 1.000000000000000000, 0.5999999999996520339, 0.3999999999996514677, 0.2999999999997390310, 0.2499999999998260003, 0.2500000000000000000),
 ( 1.000000000000000000, 0.5999999999996520339, 0.3999999999996514677, 0.2999999999997390310, 0.2499999999998260003, 0.2500000000000000000),
 ( 1.000000000000000000, 0.5999999999996520339, 0.3999999999996514677, 0.2999999999997390310, 0.2499999999998260003, 0.2500000000000000000),
 ( 1.000000000000000000, 0.5999999999996520339, 0.3999999999996514677, 0.2999999999997390310, 0.2499999999998260003, 0.2500000000000000000),
 ( 1.000000000000000000, 0.5999999999996520339, 0.3999999999996514677, 0.2999999999997390310, 0.2499999999998260003, 0.2500000000000000000),
 ( 1.000000000000000000, 0.5999999999996520339, 0.3999999999996514677, 0.2999999999997390310, 0.2499999999998260003, 0.2500000000000000000),
 ( 1.000000000000000000, 0.5999999999996520339, 0.3999999999996514677, 0.2999999999997390310, 0.2499999999998260003, 0.2500000000000000000),
 ( 1.000000000000000000, 0.5999999999996520339, 0.3999999999996514677, 0.2999999999997390310, 0.2499999999998260003, 0.2500000000000000000),
 ( 1.000000000000000000, 0.5999999999996520339, 0.3999999999996514677, 0.2999999999997390310, 0.2499999999998260003, 0.2500000000000000000),
 ( 1.000000000000000000, 0.5999999999996520339, 0.3999999999996514677, 0.2999999999997390310, 0.2499999999998260003, 0.2500000000000000000),
 ( 1.000000000000000000, 0.5999999999996520339, 0.3999999999996514677, 0.2999999999997390310, 0.2499999999998260003, 0.2500000000000000000),
 ( 1.000000000000000000, 0.5999999999996520339, 0.3999999999996514677, 0.2999999999997390310, 0.2499999999998260003, 0.2500000000000000000),
 ( 1.000000000000000000, 0.5999999999996520339, 0.3999999999996514677, 0.2999999999997390310, 0.2499999999998260003, 0.2500000000000000000),
 ( 1.000000000000000000, 0.5999999999996520339, 0.3999999999996514677, 0.2999999999997390310, 0.2499999999998260003, 0.2500000000000000000),
 ( 1.000000000000000000, 0.5999999999996520339, 0.3999999999996514677, 0.2999999999997390310, 0.2499999999998260003, 0.2500000000000000000),
 ( 1.000000000000000000, 0.5999999999996520339, 0.3999999999996514677, 0.2999999999997390310, 0.2499999999998260003, 0.2500000000000000000),
 ( 1.000000000000000000, 0.5999999999996520339, 0.3999999999996514677, 0.2999999999997390310, 0.2499999999998260003, 0.2500000000000000000),
 ( 1.000000000000000000, 0.5999999999996520339, 0.3999999999996514677, 0.2999999999997390310, 0.2499999999998260003, 0.2500000000000000000),
 ( 1.000000000000000000, 0.5999999999996520339, 0.3999999999996514677, 0.2999999999997390310, 0.2499999999998260003, 0.2500000000000000000),
 ( 1.000000000000000000, 0.5999999999996520339, 0.3999999999996514677, 0.2999999999997390310, 0.2499999999998260003, 0.2500000000000000000),
 ( 1.000000000000000000, 0.5999999999996520339, 0.3999999999996514677, 0.2999999999997390310, 0.2499999999998260003, 0.2500000000000000000),
 ( 1.000000000000000000, 0.5999999999996520339, 0.3999999999996514677, 0.2999999999997390310, 0.2499999999998260003, 0.2500000000000000000),
 ( 1.000000000000000000, 0.5999999999996520339, 0.3999999999996514677, 0.2999999999997390310, 0.2499999999998260003, 0.2500000000000000000),
 ( 1.000000000000000000, 0.5999999999996520339, 0.3999999999996514677, 0.2999999999997390310, 0.2499999999998260003, 0.2500000000000000000),
 ( 1.000000000000000000, 0.5999999999996520339, 0.3999999999996514677, 0.2999999999997390310, 0.2499999999998260003, 0.2500000000000000000),
 ( 1.000000000000000000, 0.5999999999996520339, 0.3999999999996514677, 0.2999999999997390310, 0.2499999999998260003, 0.2500000000000000000),
 ( 1.000000000000000000, 0.5999999999996520339, 0.3999999999996514677, 0.2999999999997390310, 0.2499999999998260003, 0.2500000000000000000),
 ( 1.000000000000000000, 0.5999999999996520339, 0.3999999999996514677, 0.2999999999997390310, 0.2499999999998260003, 0.2500000000000000000),
 ( 1.000000000000000000, 0.5999999999996520339, 0.3999999999996514677, 0.2999999999997390310, 0.2499999999998260003, 0.2500000000000000000),
 ( 1.000000000000000000, 0.5999999999996520339, 0.3999999999996514677, 0.2999999999997390310, 0.2499999999998260003, 0.2500000000000000000),
 ( 1.000000000000000000, 0.5999999999996520339, 0.3999999999996514677, 0.2999999999997390310, 0.2499999999998260003, 0.2500000000000000000),
 ( 1.000000000000000000, 0.5999999999996520339, 0.3999999999996514677, 0.2999999999997390310, 0.2499999999998260003, 0.2500000000000000000),
 ( 1.000000000000000000, 0.5999999999996520339, 0.3999999999996514677, 0.2999999999997390310, 0.2499999999998260003, 0.2500000000000000000),
 ( 1.000000000000000000, 0.5999999999996520339, 0.3999999999996514677, 0.2999999999997390310, 0.2499999999998260003, 0.2500000000000000000),
 ( 1.000000000000000000, 0.5999999999996520339, 0.3999999999996514677, 0.2999999999997390310, 0.2499999999998260003, 0.2500000000000000000) ) ) 
 REPRESENTATION_ITEM ( '' )  SURFACE ( )  );
#34052=DIRECTION ( 'NONE',  ( 0.8775825618903763115, 0.000000000000000000, 0.4794255386041965106 ) ) ;
#34058=CARTESIAN_POINT ( 'NONE',  ( 5.604365146370000161, 1361.139420828410039, 207.6218459616989946 ) ) ;
#34181=CARTESIAN_POINT ( 'NONE',  ( -7.992490671317017181, 1364.617306788744372, 208.3718459617061285 ) ) ;
#34190=CARTESIAN_POINT ( 'NONE',  ( -8.882606460297679973, 1368.497287369286596, 210.6218459617030021 ) ) ;
#34351=AXIS2_PLACEMENT_3D ( 'NONE', #14067, #76606, #31428 ) ;
#34467=CARTESIAN_POINT ( 'NONE',  ( 9.984115569220000097, 1365.258395869459946, 207.6218459616989946 ) ) ;
#34483=CARTESIAN_POINT ( 'NONE',  ( 8.335050544726017918, 1369.730095592100042, 209.6218459617033432 ) ) ;
#34611=CARTESIAN_POINT ( 'NONE',  ( -5.023830084653720718, 1359.755008646306578, 210.6218459617030021 ) ) ;
#34638=CARTESIAN_POINT ( 'NONE',  ( -3.005276066430000448, 1369.205039411269809, 207.6218459616989946 ) ) ;
#34731=CARTESIAN_POINT ( 'NONE',  ( -9.505471540905400474, 1363.500209798490005, 210.6218459616987957 ) ) ;
#34740=CARTESIAN_POINT ( 'NONE',  ( -9.209502321771219968, 1366.683160837834066, 210.6218459616991936 ) ) ;
#34839=FACE_OUTER_BOUND ( 'NONE', #80647, .T. ) ;
#34881=CARTESIAN_POINT ( 'NONE',  ( -1.078902958008049989E-15, 1372.293237941190000, 209.1218459616989946 ) ) ;
#35011=CARTESIAN_POINT ( 'NONE',  ( 8.001480734926794014, 1364.923464046118625, 209.6218459617148824 ) ) ;
#35017=CIRCLE ( 'NONE', #43987, 3.000000000000002665 ) ;
#35027=CARTESIAN_POINT ( 'NONE',  ( 10.10760548029105621, 1367.483665353111974, 210.6218459617030021 ) ) ;
#35039=ADVANCED_FACE ( 'NONE', ( #109468 ), #110011, .T. ) ;
#35161=CARTESIAN_POINT ( 'NONE',  ( 1.748848150589999983, 1360.440694539920059, 207.6218459616989946 ) ) ;
#35190=CARTESIAN_POINT ( 'NONE',  ( -6.559525637288459166, 1366.137815543844226, 209.6218459617148824 ) ) ;
#35269=DIRECTION ( 'NONE',  ( -5.053215498073659967E-16, -1.000000000000000000, -2.442490654180000246E-15 ) ) ;
#35270=CARTESIAN_POINT ( 'NONE',  ( -2.835036738194454564, 1367.791076339870415, 208.6398238693165297 ) ) ;
#35286=CARTESIAN_POINT ( 'NONE',  ( -8.910387285865079221, 1362.858511851195999, 210.6218459616987957 ) ) ;
#35294=CARTESIAN_POINT ( 'NONE',  ( -10.07915732761907712, 1367.514362519412089, 210.6218459617030021 ) ) ;
#35348=CARTESIAN_POINT ( 'NONE',  ( -2.860413922163684841, 1367.970058130527377, 208.1452275469912649 ) ) ;
#35562=CARTESIAN_POINT ( 'NONE',  ( 9.813910351400000565, 1364.017814053650000, 207.6218459616989946 ) ) ;
#35579=SURFACE_STYLE_USAGE ( .BOTH. , #60817 ) ;
#35581=CARTESIAN_POINT ( 'NONE',  ( 7.979399411837515999, 1369.012103654667044, 210.6218459617030021 ) ) ;
#35591=CARTESIAN_POINT ( 'NONE',  ( -8.622403150219998480, 1362.632156860360055, 207.6218459616989946 ) ) ;
#35717=CARTESIAN_POINT ( 'NONE',  ( -6.359819428916967610, 1360.120001944986825, 210.6218459617030021 ) ) ;
#35746=CARTESIAN_POINT ( 'NONE',  ( -7.408371670602375225, 1365.603856542280710, 209.6218459617148824 ) ) ;
#35831=CARTESIAN_POINT ( 'NONE',  ( -2.876093934609688763, 1368.080635615046049, 208.1320087752549455 ) ) ;
#35848=CARTESIAN_POINT ( 'NONE',  ( -8.421179885235224205, 1364.068242571890096, 210.6218459617142003 ) ) ;
#35857=CARTESIAN_POINT ( 'NONE',  ( -9.316240760817720457, 1369.171982693950895, 209.6218459617033432 ) ) ;
#35899=SURFACE_STYLE_USAGE ( .BOTH. , #18507 ) ;
#35973=COLOUR_RGB ( '', 0.40784314, 0.44705882, 0.49803922) ;
#35997=CARTESIAN_POINT ( 'NONE',  ( -7.811405798880000084, 1367.739269854439954, 210.6218459616991936 ) ) ;
#36025=TOROIDAL_SURFACE ( 'NONE', #53957, 21.40691501530000096, 1.500287545629999997 ) ;
#36032=EDGE_LOOP ( 'NONE', ( #83770, #59613 ) ) ;
#36132=CARTESIAN_POINT ( 'NONE',  ( 9.671060821812719865, 1366.060403940060041, 210.6218459616987957 ) ) ;
#36157=CARTESIAN_POINT ( 'NONE',  ( -9.351945459739999578, 1366.519103298159735, 207.6218459616989946 ) ) ;
#36175=DIRECTION ( 'NONE',  ( 0.4794255386042041156, -2.935634756405673411E-17, -0.8775825618903722036 ) ) ;
#36268=CARTESIAN_POINT ( 'NONE',  ( 7.281762805592231658, 1360.709910169842260, 207.6218459616987673 ) ) ;
#36292=CARTESIAN_POINT ( 'NONE',  ( -6.371134682384000492, 1368.423166410931799, 210.6218459616987957 ) ) ;
#36373=CARTESIAN_POINT ( 'NONE',  ( -3.007104530145896515, 1369.004598681105563, 207.6218459616999894 ) ) ;
#36388=CARTESIAN_POINT ( 'NONE',  ( -3.792994181805666276, 1361.742475207348207, 207.6218459616988241 ) ) ;
#36396=CARTESIAN_POINT ( 'NONE',  ( -5.499060144977048203, 1369.740687513229432, 207.6218459616987673 ) ) ;
#36443=CARTESIAN_POINT ( 'NONE',  ( -2.813822098188480059, 1367.641464703512383, 209.1220808600859300 ) ) ;
#36448=DIRECTION ( 'NONE',  ( -0.1403878024439498828, 0.9900965937346509760, 0.000000000000000000 ) ) ;
#36477=CARTESIAN_POINT ( 'NONE',  ( 3.855903220025218125, 1370.345307389557092, 209.9425081570149985 ) ) ;
#36540=CARTESIAN_POINT ( 'NONE',  ( -9.505471540889999460, 1363.500209798500009, 210.6218459616991936 ) ) ;
#36561=PRODUCT_DEFINITION_SHAPE ( 'NONE', 'NONE',  #25390 ) ;
#36678=CARTESIAN_POINT ( 'NONE',  ( 8.654519645408177198, 1365.419269571389577, 210.6218459617142003 ) ) ;
#36702=CARTESIAN_POINT ( 'NONE',  ( -9.516636888329999877, 1366.309137899869938, 207.6218459616989946 ) ) ;
#36709=B_SPLINE_CURVE_WITH_KNOTS ( 'NONE', 3,
 ( #71268, #44950, #1843, #88594, #28677, #79097, #53915, #11335 ),
 .UNSPECIFIED., .F., .F.,
 ( 4, 2, 2, 4 ),
 ( 0.0001365944327631960203, 0.003338885444831087533, 0.004940030950865032314, 0.006541176456898977962 ),
 .UNSPECIFIED. ) ;
#36825=CARTESIAN_POINT ( 'NONE',  ( 9.643569501056903803, 1360.898780757513578, 209.6218459617033432 ) ) ;
#36847=CARTESIAN_POINT ( 'NONE',  ( -7.004779464842641801, 1367.034864359649873, 207.6218459616988241 ) ) ;
#36878=VERTEX_POINT ( 'NONE', #29748 ) ;
#36890=EDGE_CURVE ( 'NONE', #98602, #36878, #31958, .T. ) ;
#36895=VERTEX_POINT ( 'NONE', #5666 ) ;
#36921=CARTESIAN_POINT ( 'NONE',  ( -2.866593677795437056, 1368.013634267723319, 210.0441101397873922 ) ) ;
#36941=CARTESIAN_POINT ( 'NONE',  ( -10.26707792444094736, 1367.299349508571595, 210.6218459617030021 ) ) ;
#36956=EDGE_CURVE ( 'NONE', #97580, #23634, #97533, .T. ) ;
#36990=ORIENTED_EDGE ( 'NONE', *, *, #54917, .T. ) ;
#36994=CARTESIAN_POINT ( 'NONE',  ( -2.823657736881381997, 1367.710836537829891, 208.5987421069861796 ) ) ;
#37233=CARTESIAN_POINT ( 'NONE',  ( 6.912446013178925597, 1366.858127842395334, 210.6218459617142003 ) ) ;
#37260=CARTESIAN_POINT ( 'NONE',  ( 9.093835586129998205, 1363.023136422000107, 207.6218459616989946 ) ) ;
#37380=CARTESIAN_POINT ( 'NONE',  ( 10.06893603924860869, 1361.212982179845767, 209.6218459617033432 ) ) ;
#37397=AXIS2_PLACEMENT_3D ( 'NONE', #58618, #4888, #39029 ) ;
#37405=CARTESIAN_POINT ( 'NONE',  ( -9.209502321788820112, 1366.683160837849982, 210.6218459616987957 ) ) ;
#37480=DIRECTION ( 'NONE',  ( 0.8539859765994181062, 0.000000000000000000, -0.5202960232132650686 ) ) ;
#37501=CARTESIAN_POINT ( 'NONE',  ( -10.02185219040722153, 1364.916310432309956, 210.6218459616991936 ) ) ;
#37628=CARTESIAN_POINT ( 'NONE',  ( 3.037408418089064810, 1369.431655480266272, 210.6218459616999041 ) ) ;
#37643=CARTESIAN_POINT ( 'NONE',  ( -9.934709065799999905, 1365.494406819940195, 210.6218459616991936 ) ) ;
#37786=CARTESIAN_POINT ( 'NONE',  ( 3.399663236026384538, 1367.129113533974078, 209.6218459617148824 ) ) ;
#37938=CARTESIAN_POINT ( 'NONE',  ( 7.359670431058202844, 1360.525381303870972, 210.6218459617030021 ) ) ;
#37959=CARTESIAN_POINT ( 'NONE',  ( -8.103279866443569901, 1365.019086496305590, 208.3718459617061285 ) ) ;
#38055=CARTESIAN_POINT ( 'NONE',  ( -10.32721170034283809, 1366.899502727329264, 207.6218459616987673 ) ) ;
#38187=CARTESIAN_POINT ( 'NONE',  ( 3.426613460960000079, 1360.656565846699777, 210.6218459616991936 ) ) ;
#38316=CARTESIAN_POINT ( 'NONE',  ( 8.355117317390414300, 1365.835232130580835, 210.6218459617142003 ) ) ;
#38370=CIRCLE ( 'NONE', #100940, 17.27637083661241135 ) ;
#38452=CARTESIAN_POINT ( 'NONE',  ( 4.262353028408887745, 1360.811275533914113, 210.6218459616987957 ) ) ;
#38469=CARTESIAN_POINT ( 'NONE',  ( 8.379275254589538591, 1362.454991452514150, 210.6218459616991936 ) ) ;
#38491=CARTESIAN_POINT ( 'NONE',  ( -8.123348129977994603, 1364.941198722160607, 208.3718459617061285 ) ) ;
#38571=CARTESIAN_POINT ( 'NONE',  ( -6.123233995736771213E-16, 1379.913060387289988, 209.1218459616989946 ) ) ;
#38589=CARTESIAN_POINT ( 'NONE',  ( -10.48932666274678205, 1367.017575692817445, 210.6218459617030021 ) ) ;
#38590=FACE_OUTER_BOUND ( 'NONE', #55599, .T. ) ;
#38731=CARTESIAN_POINT ( 'NONE',  ( 9.813910351400000565, 1364.017814053649772, 210.6218459616991936 ) ) ;
#38741=ORIENTED_EDGE ( 'NONE', *, *, #17901, .F. ) ;
#38770=CARTESIAN_POINT ( 'NONE',  ( -3.138284008646738954, 1369.929752808247940, 210.4427501191478882 ) ) ;
#38862=CARTESIAN_POINT ( 'NONE',  ( 4.724978704057813061, 1366.967019841526962, 208.3718459617061285 ) ) ;
#38949=CARTESIAN_POINT ( 'NONE',  ( -3.061616997868380553E-17, 1389.413060387289988, 209.1218459616989946 ) ) ;
#38994=CARTESIAN_POINT ( 'NONE',  ( -4.280544930714631491, 1362.872105239078792, 209.6218459617148824 ) ) ;
#39009=CARTESIAN_POINT ( 'NONE',  ( 10.13733714734278024, 1367.141848830506206, 207.6218459616987673 ) ) ;
#39029=DIRECTION ( 'NONE',  ( 3.828568698926945984E-16, 0.000000000000000000, -1.000000000000000000 ) ) ;
#39031=CARTESIAN_POINT ( 'NONE',  ( -9.516636888329999877, 1366.309137899869938, 207.6218459616989946 ) ) ;
#39036=CARTESIAN_POINT ( 'NONE',  ( 3.005276066430000448, 1369.205039411269809, 210.6218459616989946 ) ) ;
#39065=VERTEX_POINT ( 'NONE', #63660 ) ;
#39109=EDGE_CURVE ( 'NONE', #1227, #68445, #35017, .T. ) ;
#39135=CARTESIAN_POINT ( 'NONE',  ( -9.516636888325759713, 1366.309137899864027, 210.6218459616991936 ) ) ;
#39150=ORIENTED_EDGE ( 'NONE', *, *, #92875, .T. ) ;
#39290=CARTESIAN_POINT ( 'NONE',  ( 7.818221670729999850, 1367.736483592530021, 210.6218459616991936 ) ) ;
#39326=CARTESIAN_POINT ( 'NONE',  ( -2.864888263985923444, 1368.214942817532346, 207.6218459616988241 ) ) ;
#39337=ORIENTED_EDGE ( 'NONE', *, *, #88581, .T. ) ;
#39363=ORIENTED_EDGE ( 'NONE', *, *, #102828, .F. ) ;
#39386=TOROIDAL_SURFACE ( 'NONE', #59152, 8.000000000000000000, 2.000000000000000000 ) ;
#39418=CARTESIAN_POINT ( 'NONE',  ( 2.564995765565520003, 1366.156374150979900, 209.1218459575829911 ) ) ;
#39429=CARTESIAN_POINT ( 'NONE',  ( 5.721861508758420811, 1366.657167162936048, 208.3718459617061285 ) ) ;
#39458=CARTESIAN_POINT ( 'NONE',  ( 8.726849315049999944, 1367.111769039820047, 207.6218459616989946 ) ) ;
#39565=CARTESIAN_POINT ( 'NONE',  ( -4.745098151869999725, 1360.923919868640041, 207.6218459616989946 ) ) ;
#39582=CARTESIAN_POINT ( 'NONE',  ( 10.91522438530139638, 1365.730702465838704, 207.6218459616987673 ) ) ;
#39606=CARTESIAN_POINT ( 'NONE',  ( -9.011061020611320416, 1364.914693253510450, 207.6218459616988241 ) ) ;
#39629=CARTESIAN_POINT ( 'NONE',  ( -2.813821217590033452, 1367.641464860482529, 209.3838672787736641 ) ) ;
#39638=DIRECTION ( 'NONE',  ( -0.4794255386042042266, 2.935634756405672795E-17, 0.8775825618903720926 ) ) ;
#39705=CARTESIAN_POINT ( 'NONE',  ( -8.052217410967335454, 1361.074664824414413, 207.6218459616987673 ) ) ;
#39845=CARTESIAN_POINT ( 'NONE',  ( -3.982247585420000124, 1360.759224656429978, 210.6218459616991936 ) ) ;
#40060=VECTOR ( 'NONE', #52718, 1000.000000000000114 ) ;
#40106=CARTESIAN_POINT ( 'NONE',  ( 5.072810769355130311, 1362.944312259176513, 208.3718459617061285 ) ) ;
#40121=CARTESIAN_POINT ( 'NONE',  ( 9.842969107809999230, 1365.740588703660023, 207.6218459616989946 ) ) ;
#40149=CARTESIAN_POINT ( 'NONE',  ( -7.940837552955301248, 1365.055256626819073, 209.6218459617148824 ) ) ;
#40155=CARTESIAN_POINT ( 'NONE',  ( 2.836810703502730568, 1368.016923498806136, 210.6218459617142003 ) ) ;
#40251=CARTESIAN_POINT ( 'NONE',  ( -8.910387285859998840, 1362.858511851210096, 207.6218459616989946 ) ) ;
#40272=DIRECTION ( 'NONE',  ( 0.1403878024439506045, 0.9900965937346509760, 0.000000000000000000 ) ) ;
#40275=ORIENTED_EDGE ( 'NONE', *, *, #28124, .F. ) ;
#40385=CARTESIAN_POINT ( 'NONE',  ( 7.877099145829999038, 1362.118768394180051, 210.6218459616991936 ) ) ;
#40414=CARTESIAN_POINT ( 'NONE',  ( -2.155023191118941472, 1370.176848074955160, 211.3933356164083364 ) ) ;
#40418=CARTESIAN_POINT ( 'NONE',  ( -3.763781937373404052, 1369.097489338571904, 210.6218459616987957 ) ) ;
#40518=EDGE_CURVE ( 'NONE', #101372, #23634, #23613, .T. ) ;
#40595=CARTESIAN_POINT ( 'NONE',  ( -3.323881039096373335, 1370.249599412167072, 210.1653830766376245 ) ) ;
#40596=AXIS2_PLACEMENT_3D ( 'NONE', #54405, #39638, #54942 ) ;
#40660=CARTESIAN_POINT ( 'NONE',  ( 8.050322358089076147, 1364.710190515749900, 208.3718459617061285 ) ) ;
#40676=CARTESIAN_POINT ( 'NONE',  ( 9.925983360904959696, 1364.303202023269932, 210.6218459616991936 ) ) ;
#40803=CARTESIAN_POINT ( 'NONE',  ( -9.505471540889999460, 1363.500209798499782, 207.6218459616989946 ) ) ;
#40999=VERTEX_POINT ( 'NONE', #31663 ) ;
#41059=EDGE_CURVE ( 'NONE', #68445, #78057, #110697, .T. ) ;
#41073=DIRECTION ( 'NONE',  ( 1.192122195693504081E-14, -4.372198439846870180E-16, -1.000000000000000000 ) ) ;
#41112=CARTESIAN_POINT ( 'NONE',  ( -5.599233173528683771, 1387.285800435509827, 209.1218459616989946 ) ) ;
#41216=CARTESIAN_POINT ( 'NONE',  ( 7.340269731169999368, 1361.836778001489847, 207.6218459616989946 ) ) ;
#41233=CARTESIAN_POINT ( 'NONE',  ( 9.984115569218559472, 1365.258395869460173, 210.6218459616991936 ) ) ;
#41369=CARTESIAN_POINT ( 'NONE',  ( -10.03857228576058702, 1362.268081971562196, 210.6218459617030021 ) ) ;
#41391=DIRECTION ( 'NONE',  ( 0.9900965937346507539, -0.1403878024439509931, 3.790652827686679061E-16 ) ) ;
#41532=CARTESIAN_POINT ( 'NONE',  ( 1.065212260669379907, 1370.038499060255617, 211.2582246529558745 ) ) ;
#41759=CARTESIAN_POINT ( 'NONE',  ( 7.314476403582760078, 1363.998884265407241, 208.3718459617061285 ) ) ;
#41777=CARTESIAN_POINT ( 'NONE',  ( 10.60049277610792373, 1367.947287196954221, 208.3718459617010978 ) ) ;
#41916=CARTESIAN_POINT ( 'NONE',  ( -9.651661623395108691, 1361.059646503146041, 208.3718459617010978 ) ) ;
#41932=CARTESIAN_POINT ( 'NONE',  ( -9.491012693391989759E-16, 1374.413060387289988, 209.1218459616989946 ) ) ;
#42022=DIRECTION ( 'NONE',  ( -0.8775825618903722036, 0.000000000000000000, -0.4794255386042038936 ) ) ;
#42038=CARTESIAN_POINT ( 'NONE',  ( -8.059861619861480975, 1364.726888446574776, 208.3718459617061285 ) ) ;
#42074=DIRECTION ( 'NONE',  ( -6.123233995736769734E-17, -1.000000000000000000, -1.124819836996389922E-32 ) ) ;
#42256=CARTESIAN_POINT ( 'NONE',  ( -4.409129114201552291, 1370.458449300261009, 208.8325715886037983 ) ) ;
#42313=CARTESIAN_POINT ( 'NONE',  ( 9.663424421700000266, 1363.752474719049815, 207.6218459616989946 ) ) ;
#42328=DIRECTION ( 'NONE',  ( 1.000000000000000000, 0.000000000000000000, 0.000000000000000000 ) ) ;
#42330=CARTESIAN_POINT ( 'NONE',  ( 10.90489178456198793, 1367.786170745731170, 209.6218459617033432 ) ) ;
#42396=DIRECTION ( 'NONE',  ( -3.828568698926946970E-16, 0.000000000000000000, 1.000000000000000000 ) ) ;
#42457=CARTESIAN_POINT ( 'NONE',  ( 4.644984669262973043, 1358.972932498876844, 208.3718459617010978 ) ) ;
#42586=CARTESIAN_POINT ( 'NONE',  ( -7.107332553001914910, 1363.850055010189408, 208.3718459617061285 ) ) ;
#42593=CARTESIAN_POINT ( 'NONE',  ( -9.317611367242571774, 1367.919873931656866, 207.6218459616987673 ) ) ;
#42618=PRODUCT_CONTEXT ( 'NONE', #5534, 'mechanical' ) ;
#42630=DIRECTION ( 'NONE',  ( 0.9900962604114871279, -0.1403901532130690244, 1.186453863995930381E-14 ) ) ;
#42733=CARTESIAN_POINT ( 'NONE',  ( -0.9985785836218079581, 1368.656171449427575, 210.4211784751752248 ) ) ;
#42767=ORIENTED_EDGE ( 'NONE', *, *, #51511, .F. ) ;
#42792=CARTESIAN_POINT ( 'NONE',  ( 8.337034337958536767, 1374.913060387289988, 213.6763885784389174 ) ) ;
#42877=CARTESIAN_POINT ( 'NONE',  ( 7.930617565348595299, 1365.289423324231848, 208.3718459617061285 ) ) ;
#42890=DIRECTION ( 'NONE',  ( 0.000000000000000000, 0.000000000000000000, 1.000000000000000000 ) ) ;
#42892=CARTESIAN_POINT ( 'NONE',  ( 10.69176820126198280, 1368.033143093960234, 209.6218459617033432 ) ) ;
#42960=DIRECTION ( 'NONE',  ( -6.123233995736769734E-17, -1.000000000000000000, -1.124819836996399911E-32 ) ) ;
#43021=CARTESIAN_POINT ( 'NONE',  ( -3.071538966616303767, 1375.413060387289988, 207.4438565765842952 ) ) ;
#43027=CARTESIAN_POINT ( 'NONE',  ( 0.06125050287350902040, 1359.189416546558277, 210.6218459617030021 ) ) ;
#43053=CARTESIAN_POINT ( 'NONE',  ( -3.005276066433927973, 1369.205039411293910, 210.6218459616987957 ) ) ;
#43084=CARTESIAN_POINT ( 'NONE',  ( 3.067412410608044926, 1369.643261120324723, 207.6621350963564225 ) ) ;
#43147=CARTESIAN_POINT ( 'NONE',  ( -8.798121132677117373, 1364.254821810437306, 207.6218459616988241 ) ) ;
#43156=CARTESIAN_POINT ( 'NONE',  ( -8.340540947510188374, 1369.726010807078183, 209.6218459617033432 ) ) ;
#43267=VECTOR ( 'NONE', #84167, 999.9999999999998863 ) ;
#43431=CARTESIAN_POINT ( 'NONE',  ( 8.808881355756348341, 1364.900047799910453, 210.6218459617142003 ) ) ;
#43444=( LENGTH_UNIT ( ) NAMED_UNIT ( * ) SI_UNIT ( .MILLI., .METRE. ) );
#43446=CARTESIAN_POINT ( 'NONE',  ( 9.353206833242573737, 1367.891569019600183, 207.6218459616987673 ) ) ;
#43458=CARTESIAN_POINT ( 'NONE',  ( -9.209502321770001387, 1366.683160837839978, 207.6218459616989946 ) ) ;
#43488=EDGE_CURVE ( 'NONE', #23634, #88920, #77535, .T. ) ;
#43577=CARTESIAN_POINT ( 'NONE',  ( -4.337097717182941459, 1358.915629873471289, 208.3718459617010978 ) ) ;
#43602=CARTESIAN_POINT ( 'NONE',  ( -4.517103279549999684, 1368.953374755989898, 207.6218459616989946 ) ) ;
#43694=CARTESIAN_POINT ( 'NONE',  ( -6.729522994862413121, 1363.632850206206285, 208.3718459617061285 ) ) ;
#43702=CARTESIAN_POINT ( 'NONE',  ( -9.632230605042634508, 1367.664641040586275, 207.6218459616987673 ) ) ;
#43962=CARTESIAN_POINT ( 'NONE',  ( 3.145310910306181373, 1370.220870732725871, 208.0282141261312461 ) ) ;
#43981=CARTESIAN_POINT ( 'NONE',  ( 9.704582620035441920, 1366.001145740646052, 210.6218459616987957 ) ) ;
#43987=AXIS2_PLACEMENT_3D ( 'NONE', #22236, #99503, #105741 ) ;
#43997=CARTESIAN_POINT ( 'NONE',  ( 9.339950631061057607, 1369.158344092944390, 209.6218459617033432 ) ) ;
#44007=CARTESIAN_POINT ( 'NONE',  ( 8.476942927299997876, 1362.523913559720086, 207.6218459616989946 ) ) ;
#44134=CARTESIAN_POINT ( 'NONE',  ( -4.360754392635079135, 1358.792723554605345, 209.6218459617033432 ) ) ;
#44159=CARTESIAN_POINT ( 'NONE',  ( -4.105920213440668931, 1367.121443183097654, 208.3718459617061285 ) ) ;
#44256=CARTESIAN_POINT ( 'NONE',  ( -8.622403150219998480, 1362.632156860360055, 207.6218459616989946 ) ) ;
#44264=CARTESIAN_POINT ( 'NONE',  ( -8.297911554434026726, 1368.614765545475393, 207.6218459616987673 ) ) ;
#44406=CARTESIAN_POINT ( 'NONE',  ( -9.690020260109999839, 1366.026910387849966, 210.6218459616991936 ) ) ;
#44462=CARTESIAN_POINT ( 'NONE',  ( -3.088437838665793578, 1369.578208569719209, 207.6586240303519162 ) ) ;
#44535=CARTESIAN_POINT ( 'NONE',  ( 7.945025989411964140, 1365.048221891109279, 209.6218459617148824 ) ) ;
#44559=CARTESIAN_POINT ( 'NONE',  ( -4.745098151869999725, 1360.923919868640041, 207.6218459616989946 ) ) ;
#44692=CARTESIAN_POINT ( 'NONE',  ( -0.8296751164775166831, 1358.402594231689591, 209.6218459617033432 ) ) ;
#44700=LINE ( 'NONE', #79394, #57339 ) ;
#44719=CARTESIAN_POINT ( 'NONE',  ( -7.215824617674233998, 1365.903927215113299, 208.3718459617061285 ) ) ;
#44729=EDGE_CURVE ( 'NONE', #39065, #25781, #3377, .T. ) ;
#44815=CARTESIAN_POINT ( 'NONE',  ( 5.037373810890384718, 1363.064638354549515, 209.6218459617148824 ) ) ;
#44825=CARTESIAN_POINT ( 'NONE',  ( -7.450033292399999674, 1367.931913175460068, 207.6218459616989946 ) ) ;
#44896=ORIENTED_EDGE ( 'NONE', *, *, #3684, .T. ) ;
#44912=CARTESIAN_POINT ( 'NONE',  ( 4.107457091549650663, 1370.394943853835002, 209.7763353197741480 ) ) ;
#44950=CARTESIAN_POINT ( 'NONE',  ( -2.162165485562111300, 1370.150135755310203, 206.8746041456742830 ) ) ;
#45028=DIRECTION ( 'NONE',  ( -6.123233995736769734E-17, -1.000000000000000000, -1.124819836996389922E-32 ) ) ;
#45032=( GEOMETRIC_REPRESENTATION_CONTEXT ( 3 ) GLOBAL_UNCERTAINTY_ASSIGNED_CONTEXT ( ( #8778 ) ) GLOBAL_UNIT_ASSIGNED_CONTEXT ( ( #93807, #67553, #101655 ) ) REPRESENTATION_CONTEXT ( 'NONE', 'WORKASPACE' ) );
#45105=CARTESIAN_POINT ( 'NONE',  ( 7.954477662311944641, 1365.031352125213971, 209.6218459617148824 ) ) ;
#45128=CARTESIAN_POINT ( 'NONE',  ( -9.690020260109999839, 1366.026910387849966, 207.6218459616989946 ) ) ;
#45250=CARTESIAN_POINT ( 'NONE',  ( 7.773062682075623897, 1360.933485754074582, 207.6218459616987673 ) ) ;
#45275=CARTESIAN_POINT ( 'NONE',  ( -7.450033292399999674, 1367.931913175460068, 207.6218459616989946 ) ) ;
#45356=CARTESIAN_POINT ( 'NONE',  ( -2.824334885622032054, 1367.715600639032345, 209.0250458202570201 ) ) ;
#45379=CARTESIAN_POINT ( 'NONE',  ( -9.830395177430180098, 1365.769828494181866, 210.6218459616991936 ) ) ;
#45523=EDGE_CURVE ( 'NONE', #27860, #98602, #69417, .T. ) ;
#45620=CARTESIAN_POINT ( 'NONE',  ( -1.331958139231829923E-15, 1375.413060387289988, 209.1218459616989946 ) ) ;
#45660=CARTESIAN_POINT ( 'NONE',  ( 4.953742833043618177, 1367.812870383251266, 207.6218459616988241 ) ) ;
#45685=CARTESIAN_POINT ( 'NONE',  ( 4.262353028419999745, 1360.811275533920025, 207.6218459616989946 ) ) ;
#45804=CARTESIAN_POINT ( 'NONE',  ( 7.859621272268051406, 1360.752827304597304, 210.6218459617030021 ) ) ;
#45825=CARTESIAN_POINT ( 'NONE',  ( -8.696701630030000629, 1367.135748871429996, 207.6218459616989946 ) ) ;
#45861=AXIS2_PLACEMENT_3D ( 'NONE', #105803, #35269, #37480 ) ;
#45917=CARTESIAN_POINT ( 'NONE',  ( -10.75519305779300616, 1363.664311205124022, 207.6218459616987673 ) ) ;
#45952=ORIENTED_EDGE ( 'NONE', *, *, #24333, .F. ) ;
#46134=CARTESIAN_POINT ( 'NONE',  ( -3.161014919395765510, 1370.090064437274350, 207.9054318704831985 ) ) ;
#46205=CARTESIAN_POINT ( 'NONE',  ( 6.844085095878397418, 1365.985930475517080, 209.6218459617148824 ) ) ;
#46223=CARTESIAN_POINT ( 'NONE',  ( -9.184850993605149917E-16, 1374.913060387289988, 209.1218459616989946 ) ) ;
#46234=CARTESIAN_POINT ( 'NONE',  ( 8.251048879689999893, 1367.474174444410210, 207.6218459616989946 ) ) ;
#46357=CARTESIAN_POINT ( 'NONE',  ( 8.370313053925706015, 1361.245476951179626, 207.6218459616987673 ) ) ;
#46382=CARTESIAN_POINT ( 'NONE',  ( -7.996809115789493383, 1365.202203848373529, 208.3718459617061285 ) ) ;
#46403=CARTESIAN_POINT ( 'NONE',  ( -2.823654301615894369, 1367.710812309479252, 209.6453303274731468 ) ) ;
#46478=CARTESIAN_POINT ( 'NONE',  ( -9.978586514373580130, 1364.539968386208102, 210.6218459616991936 ) ) ;
#46555=CARTESIAN_POINT ( 'NONE',  ( 4.473673856261621395, 1370.472484186452448, 209.0519328995294472 ) ) ;
#46622=CARTESIAN_POINT ( 'NONE',  ( 9.943976501839999926, 1365.461622992590037, 210.6218459616991936 ) ) ;
#46757=CARTESIAN_POINT ( 'NONE',  ( 8.251048879710380035, 1367.474174444426126, 210.6218459616987957 ) ) ;
#46772=CARTESIAN_POINT ( 'NONE',  ( 4.090111291624164203, 1370.944973062717054, 208.3718459617010978 ) ) ;
#46877=EDGE_CURVE ( 'NONE', #32551, #9968, #92635, .T. ) ;
#46889=CARTESIAN_POINT ( 'NONE',  ( 1.670893000356252323, 1361.439592909522844, 207.6218459616988241 ) ) ;
#46906=CARTESIAN_POINT ( 'NONE',  ( 8.151756514128491560, 1360.143105037590431, 208.3718459617010978 ) ) ;
#46930=CARTESIAN_POINT ( 'NONE',  ( -10.02185219039999886, 1364.916310432309956, 207.6218459616989946 ) ) ;
#47021=CARTESIAN_POINT ( 'NONE',  ( -11.83375927753976065, 1364.194490855938511, 208.3718459617010978 ) ) ;
#47155=CARTESIAN_POINT ( 'NONE',  ( 9.704582620010000937, 1366.001145740639913, 210.6218459616991936 ) ) ;
#47222=DIRECTION ( 'NONE',  ( -6.123233995736769734E-17, -1.000000000000000000, -1.124819836996399911E-32 ) ) ;
#47283=CARTESIAN_POINT ( 'NONE',  ( 8.501157997614470219, 1365.972601565777268, 207.6218459616988241 ) ) ;
#47423=CARTESIAN_POINT ( 'NONE',  ( -4.512821541280432669, 1361.898012553873741, 207.6218459616988241 ) ) ;
#47427=EDGE_LOOP ( 'NONE', ( #13844, #107478, #102362, #22652 ) ) ;
#47439=CARTESIAN_POINT ( 'NONE',  ( 10.40445411670284415, 1362.691325679774536, 210.6218459617030021 ) ) ;
#47465=CARTESIAN_POINT ( 'NONE',  ( -8.543947113920394187, 1365.600700106919930, 210.6218459617142003 ) ) ;
#47470=CARTESIAN_POINT ( 'NONE',  ( 3.005276066430000448, 1369.205039411269809, 207.6218459616989946 ) ) ;
#47499=CARTESIAN_POINT ( 'NONE',  ( 3.071538966616300659, 1375.413060387289988, 210.7998353468136941 ) ) ;
#47530=ORIENTED_EDGE ( 'NONE', *, *, #104492, .T. ) ;
#47562=CARTESIAN_POINT ( 'NONE',  ( -9.351945459727259546, 1366.519103298152004, 210.6218459616991936 ) ) ;
#47702=CARTESIAN_POINT ( 'NONE',  ( 9.231361398829999843, 1366.659448741839924, 210.6218459616991936 ) ) ;
#47833=CARTESIAN_POINT ( 'NONE',  ( 8.312847552073090895, 1366.156914216811174, 207.6218459616988241 ) ) ;
#47965=CARTESIAN_POINT ( 'NONE',  ( 5.264170345090959380, 1362.294551344075671, 210.6218459617142003 ) ) ;
#47985=CARTESIAN_POINT ( 'NONE',  ( 10.97628319970143274, 1365.429341111210306, 207.6218459616987673 ) ) ;
#48009=CARTESIAN_POINT ( 'NONE',  ( -9.977700672476359500, 1365.292605733893879, 210.6218459616987957 ) ) ;
#48043=ORIENTED_EDGE ( 'NONE', *, *, #88581, .F. ) ;
#48116=CARTESIAN_POINT ( 'NONE',  ( -9.057796188674942073, 1360.633927564615988, 208.3718459617010978 ) ) ;
#48147=ORIENTED_EDGE ( 'NONE', *, *, #63757, .F. ) ;
#48192=EDGE_LOOP ( 'NONE', ( #22462, #14593, #83379, #63983, #103758, #102708, #33331, #30786 ) ) ;
#48200=CARTESIAN_POINT ( 'NONE',  ( 3.719802410872147913, 1370.319534414420104, 210.0106693369416178 ) ) ;
#48302=ADVANCED_FACE ( 'NONE', ( #106426 ), #14055, .T. ) ;
#48399=CARTESIAN_POINT ( 'NONE',  ( 2.864888263985923444, 1368.214942817532346, 207.6218459616988241 ) ) ;
#48409=CARTESIAN_POINT ( 'NONE',  ( -9.491012693391989759E-16, 1374.413060387289988, 209.1218459616989946 ) ) ;
#48439=EDGE_CURVE ( 'NONE', #53641, #96281, #60619, .T. ) ;
#48469=CARTESIAN_POINT ( 'NONE',  ( -4.459845537155718631, 1370.469452523700738, 208.9750888997069467 ) ) ;
#48530=MECHANICAL_DESIGN_GEOMETRIC_PRESENTATION_REPRESENTATION('',(#9198),#45032);
#48531=CARTESIAN_POINT ( 'NONE',  ( -0.6941066948465304254, 1362.404256174842203, 209.6218459617148824 ) ) ;
#48535=ORIENTED_EDGE ( 'NONE', *, *, #18154, .T. ) ;
#48549=CARTESIAN_POINT ( 'NONE',  ( 11.73111152208969798, 1363.746748086613479, 208.3718459617010978 ) ) ;
#48573=CARTESIAN_POINT ( 'NONE',  ( -8.808902786682349273, 1364.914369817750185, 210.6218459617142003 ) ) ;
#48619=ADVANCED_FACE ( 'NONE', ( #73934 ), #87462, .T. ) ;
#48661=FACE_OUTER_BOUND ( 'NONE', #96914, .T. ) ;
#48679=CARTESIAN_POINT ( 'NONE',  ( -11.11931780176117179, 1362.308639675578434, 209.6218459617033432 ) ) ;
#48756=CARTESIAN_POINT ( 'NONE',  ( 3.295895095316650814, 1370.244911477964024, 210.1744081590250630 ) ) ;
#48780=CYLINDRICAL_SURFACE ( 'NONE', #62211, 2.999999999999999556 ) ;
#48818=CARTESIAN_POINT ( 'NONE',  ( 7.340269731169999368, 1361.836778001490075, 210.6218459616991936 ) ) ;
#49082=CARTESIAN_POINT ( 'NONE',  ( 8.631039101008498804, 1364.365412828926765, 210.6218459617142003 ) ) ;
#49098=CARTESIAN_POINT ( 'NONE',  ( 11.08126538406277461, 1363.947071503807592, 210.6218459617030021 ) ) ;
#49144=DIRECTION ( 'NONE',  ( -6.123233995736769734E-17, -1.000000000000000000, -1.124819836996399911E-32 ) ) ;
#49226=CARTESIAN_POINT ( 'NONE',  ( -11.43307569840619387, 1362.816133835241999, 209.6218459617033432 ) ) ;
#49567=CARTESIAN_POINT ( 'NONE',  ( -3.467356662694556668, 1370.274142583225967, 208.1271013349179100 ) ) ;
#49630=CARTESIAN_POINT ( 'NONE',  ( 6.820918190075792253, 1362.920728698377161, 210.6218459617142003 ) ) ;
#49646=CARTESIAN_POINT ( 'NONE',  ( 9.369782510130001185, 1366.497526915280105, 207.6218459616989946 ) ) ;
#49770=DIRECTION ( 'NONE',  ( -0.4794255386042040046, 2.935634756405673411E-17, 0.8775825618903723147 ) ) ;
#49774=CARTESIAN_POINT ( 'NONE',  ( -8.706712734255761532, 1361.212830504819522, 210.6218459617030021 ) ) ;
#49838=EDGE_LOOP ( 'NONE', ( #64298, #39337, #97041, #70405 ) ) ;
#49937=AXIS2_PLACEMENT_3D ( 'NONE', #16234, #66691, #42022 ) ;
#49957=CARTESIAN_POINT ( 'NONE',  ( -6.123233995736771213E-16, 1379.913060387289988, 209.1218459616989946 ) ) ;
#50048=DIRECTION ( 'NONE',  ( -6.123233995736769734E-17, -1.000000000000000000, -1.124819836996399911E-32 ) ) ;
#50121=CARTESIAN_POINT ( 'NONE',  ( -4.472278223723283652, 1370.472180122668533, 209.2025140426527230 ) ) ;
#50188=CARTESIAN_POINT ( 'NONE',  ( 9.258247136812819633, 1363.198586359113960, 210.6218459616987957 ) ) ;
#50204=CARTESIAN_POINT ( 'NONE',  ( 8.988338641398978979, 1366.896325247141931, 210.6218459616991936 ) ) ;
#50224=DIRECTION ( 'NONE',  ( 3.828568698926946970E-16, 0.000000000000000000, -1.000000000000000000 ) ) ;
#50281=ORIENTED_EDGE ( 'NONE', *, *, #7636, .F. ) ;
#50339=CARTESIAN_POINT ( 'NONE',  ( -11.26379070871446331, 1362.773408316262476, 208.3718459617010978 ) ) ;
#50455=CARTESIAN_POINT ( 'NONE',  ( -8.622403150232841540, 1362.632156860344139, 210.6218459616987957 ) ) ;
#50618=ORIENTED_EDGE ( 'NONE', *, *, #24333, .T. ) ;
#50717=CARTESIAN_POINT ( 'NONE',  ( 9.622136349630000751, 1363.684386430210225, 207.6218459616989946 ) ) ;
#50730=CARTESIAN_POINT ( 'NONE',  ( 9.369782510132241171, 1366.497526915279877, 210.6218459616991936 ) ) ;
#50870=CARTESIAN_POINT ( 'NONE',  ( 0.06074730888943565693, 1359.389611325063242, 207.6218459616987673 ) ) ;
#50992=CARTESIAN_POINT ( 'NONE',  ( 3.005276066430000448, 1369.205039411269809, 210.6218459616989946 ) ) ;
#50996=CARTESIAN_POINT ( 'NONE',  ( -8.082564370853681623, 1362.241991287382007, 210.6218459616987957 ) ) ;
#51004=CARTESIAN_POINT ( 'NONE',  ( -4.780260440829766644, 1370.125810961987781, 210.6218459617030021 ) ) ;
#51034=CARTESIAN_POINT ( 'NONE',  ( -1.090665124220995930, 1370.067406900570404, 211.2860174477949613 ) ) ;
#51176=DIRECTION ( 'NONE',  ( 0.9900965937346509760, 0.1403878024439500216, 3.790652827686680047E-16 ) ) ;
#51213=DIRECTION ( 'NONE',  ( 0.8775825618903720926, 0.000000000000000000, 0.4794255386042039491 ) ) ;
#51266=CARTESIAN_POINT ( 'NONE',  ( 9.093835586129998205, 1363.023136422000107, 207.6218459616989946 ) ) ;
#51280=CARTESIAN_POINT ( 'NONE',  ( 8.904389930515678842, 1368.484676233528489, 210.6218459617030021 ) ) ;
#51417=CARTESIAN_POINT ( 'NONE',  ( 6.892224678239999847, 1361.632554499750086, 207.6218459616989946 ) ) ;
#51511=EDGE_CURVE ( 'NONE', #69033, #1227, #86031, .T. ) ;
#51542=CARTESIAN_POINT ( 'NONE',  ( -8.910387285859998840, 1362.858511851210096, 207.6218459616989946 ) ) ;
#51551=CARTESIAN_POINT ( 'NONE',  ( -8.774197885167456690, 1368.328613538127001, 207.6218459616987673 ) ) ;
#51834=CARTESIAN_POINT ( 'NONE',  ( 8.000294350727555681, 1364.913589071355318, 209.6218459617148824 ) ) ;
#51849=CARTESIAN_POINT ( 'NONE',  ( 8.402703615647871160, 1368.786815462734921, 210.6218459617030021 ) ) ;
#51860=CARTESIAN_POINT ( 'NONE',  ( -6.376409808257103684, 1368.420764496007678, 207.6218459616990231 ) ) ;
#51980=CARTESIAN_POINT ( 'NONE',  ( -0.7618909056700008398, 1360.403425203260213, 207.6218459616989946 ) ) ;
#52005=CARTESIAN_POINT ( 'NONE',  ( -7.760077312028009544, 1365.297824701876380, 209.6218459617148824 ) ) ;
#52089=CARTESIAN_POINT ( 'NONE',  ( -2.895732582093412333, 1368.219138801509644, 210.2516770323846629 ) ) ;
#52105=CARTESIAN_POINT ( 'NONE',  ( -7.042317098485010973, 1363.957259258367230, 209.6218459617148824 ) ) ;
#52113=CARTESIAN_POINT ( 'NONE',  ( -8.395212705517364427, 1368.789864683679070, 210.6218459617030021 ) ) ;
#52397=CARTESIAN_POINT ( 'NONE',  ( 8.731338020832811964, 1365.274321608607124, 210.6218459617142003 ) ) ;
#52409=CARTESIAN_POINT ( 'NONE',  ( 9.389216481230956646, 1368.118150840410408, 210.6218459617030021 ) ) ;
#52419=CARTESIAN_POINT ( 'NONE',  ( -8.910387285859998840, 1362.858511851210096, 207.6218459616989946 ) ) ;
#52534=CARTESIAN_POINT ( 'NONE',  ( -8.006252579206014630, 1359.935925956307983, 209.6218459617033432 ) ) ;
#52548=VERTEX_POINT ( 'NONE', #79351 ) ;
#52562=CARTESIAN_POINT ( 'NONE',  ( -6.915728699340433216, 1366.855454596503250, 210.6218459617142003 ) ) ;
#52612=CIRCLE ( 'NONE', #68770, 2.500000000000002220 ) ;
#52654=CARTESIAN_POINT ( 'NONE',  ( -6.757614358386126341, 1362.669000810187299, 207.6218459616988241 ) ) ;
#52662=CARTESIAN_POINT ( 'NONE',  ( -3.763781937369067965, 1369.097489338547803, 210.6218459616991936 ) ) ;
#52705=PRESENTATION_STYLE_ASSIGNMENT (( #35899 ) ) ;
#52718=DIRECTION ( 'NONE',  ( 0.1215792179600219541, -0.8574474952671515826, -0.5000022866150888312 ) ) ;
#52764=DIRECTION ( 'NONE',  ( -0.8775825618903720926, 0.000000000000000000, -0.4794255386042041156 ) ) ;
#52922=CARTESIAN_POINT ( 'NONE',  ( -8.775825618903738246, 1374.413060387289988, 204.3275905756569841 ) ) ;
#52940=CARTESIAN_POINT ( 'NONE',  ( 8.122886720353145407, 1364.957098980272804, 208.3718459617061285 ) ) ;
#52969=CARTESIAN_POINT ( 'NONE',  ( 7.340269731169999368, 1361.836778001489847, 207.6218459616989946 ) ) ;
#53022=LINE ( 'NONE', #26122, #69735 ) ;
#53090=CARTESIAN_POINT ( 'NONE',  ( -5.180616796779289324, 1359.097496083801843, 208.3718459617010978 ) ) ;
#53117=CARTESIAN_POINT ( 'NONE',  ( -4.253946116614677919, 1367.780938548775339, 210.6218459617142003 ) ) ;
#53193=CARTESIAN_POINT ( 'NONE',  ( -2.867396511858420372, 1368.019296321386491, 208.2077839524759781 ) ) ;
#53211=CARTESIAN_POINT ( 'NONE',  ( -4.745098151936928410, 1360.923919868569783, 210.6218459616987957 ) ) ;
#53221=CARTESIAN_POINT ( 'NONE',  ( -3.978066776185401388, 1370.279108416835925, 210.6218459617030021 ) ) ;
#53279=DIRECTION ( 'NONE',  ( 0.9900965937346509760, 0.1403878024439500216, 3.790652827686680047E-16 ) ) ;
#53329=AXIS2_PLACEMENT_3D ( 'NONE', #95428, #78067, #51213 ) ;
#53362=CARTESIAN_POINT ( 'NONE',  ( -9.351945459730000465, 1366.519103298159962, 210.6218459616991936 ) ) ;
#53499=CARTESIAN_POINT ( 'NONE',  ( 9.943976501839999926, 1365.461622992600041, 207.6218459616989946 ) ) ;
#53505=AXIS2_PLACEMENT_3D ( 'NONE', #63358, #12354, #100230 ) ;
#53525=CARTESIAN_POINT ( 'NONE',  ( -8.538839991170000587, 1362.569232148550100, 207.6218459616989946 ) ) ;
#53641=VERTEX_POINT ( 'NONE', #92354 ) ;
#53654=CARTESIAN_POINT ( 'NONE',  ( 9.622136349625579399, 1363.684386430212044, 210.6218459616991936 ) ) ;
#53685=CARTESIAN_POINT ( 'NONE',  ( -7.148069258222480293, 1365.798506070639633, 209.6218459617148824 ) ) ;
#53782=CARTESIAN_POINT ( 'NONE',  ( 0.05823133897989880153, 1360.390585217559874, 207.6218459616989946 ) ) ;
#53791=CARTESIAN_POINT ( 'NONE',  ( -11.03264336018479774, 1364.917927611109917, 207.6218459616987673 ) ) ;
#53835=EDGE_CURVE ( 'NONE', #60506, #77151, #91818, .T. ) ;
#53915=CARTESIAN_POINT ( 'NONE',  ( 2.641027167160353795, 1370.251786685222896, 206.7745814587238158 ) ) ;
#53957=AXIS2_PLACEMENT_3D ( 'NONE', #109610, #33425, #24475 ) ;
#54064=CARTESIAN_POINT ( 'NONE',  ( 8.793514412655110135, 1365.053261579362697, 210.6218459617142003 ) ) ;
#54091=CARTESIAN_POINT ( 'NONE',  ( -9.978586514379999883, 1364.539968386210148, 207.6218459616989946 ) ) ;
#54209=CARTESIAN_POINT ( 'NONE',  ( 11.38406662287786908, 1362.730911202566858, 209.6218459617033432 ) ) ;
#54232=CARTESIAN_POINT ( 'NONE',  ( -7.450033292409739438, 1367.931913175477803, 210.6218459616987957 ) ) ;
#54332=CARTESIAN_POINT ( 'NONE',  ( -10.87716623425449569, 1367.819513648856628, 209.6218459617033432 ) ) ;
#54405=CARTESIAN_POINT ( 'NONE',  ( 7.020660495122974076, 1374.031200045389824, 212.9572502705326258 ) ) ;
#54415=CARTESIAN_POINT ( 'NONE',  ( 3.724606435798804682, 1370.320419915130969, 208.2352337144575074 ) ) ;
#54477=CARTESIAN_POINT ( 'NONE',  ( -9.209502321770001387, 1366.683160837839978, 210.6218459616991936 ) ) ;
#54500=PRODUCT ( 'Handle Screw', 'Handle Screw', '', ( #42618 ) ) ;
#54609=CARTESIAN_POINT ( 'NONE',  ( 5.215187551879999717, 1368.779556716650177, 207.6218459616989946 ) ) ;
#54624=CARTESIAN_POINT ( 'NONE',  ( 3.286051671319225598, 1371.185232598742687, 209.6218459617033432 ) ) ;
#54642=AXIS2_PLACEMENT_3D ( 'NONE', #74533, #58821, #6200 ) ;
#54753=CARTESIAN_POINT ( 'NONE',  ( 10.52374552228457105, 1363.241692960809132, 207.6218459616987673 ) ) ;
#54759=DIRECTION ( 'NONE',  ( -0.1215792179600209827, -0.8574474952671518047, -0.5000022866150889422 ) ) ;
#54771=CARTESIAN_POINT ( 'NONE',  ( -8.647453749692138203, 1364.394047320720802, 210.6218459617142003 ) ) ;
#54873=CARTESIAN_POINT ( 'NONE',  ( -10.90152747735140615, 1365.778415155553830, 207.6218459616987673 ) ) ;
#54874=DIRECTION ( 'NONE',  ( 0.9900965937346510870, 0.1403878024439500494, 3.790652827686684978E-16 ) ) ;
#54917=EDGE_CURVE ( 'NONE', #52548, #32037, #27208, .T. ) ;
#54942=DIRECTION ( 'NONE',  ( 0.8775825618903703162, 0.000000000000000000, 0.4794255386042073908 ) ) ;
#55006=CARTESIAN_POINT ( 'NONE',  ( 3.126158272763291279, 1370.057571174347913, 210.3709297514385810 ) ) ;
#55158=CARTESIAN_POINT ( 'NONE',  ( 8.653423937804200605, 1367.169888897642068, 210.6218459616987957 ) ) ;
#55172=CARTESIAN_POINT ( 'NONE',  ( 4.112383809545077540, 1371.068065305577647, 209.6218459617033432 ) ) ;
#55300=CARTESIAN_POINT ( 'NONE',  ( 10.73349977660030419, 1361.841353345481366, 209.6218459617033432 ) ) ;
#55323=CARTESIAN_POINT ( 'NONE',  ( -9.657355732032620210, 1366.083296228059908, 210.6218459616987957 ) ) ;
#55418=CARTESIAN_POINT ( 'NONE',  ( -11.23480159415162127, 1364.918251046870182, 210.6218459617030021 ) ) ;
#55422=AXIS2_PLACEMENT_3D ( 'NONE', #17477, #93105, #8001 ) ;
#55513=B_SPLINE_CURVE_WITH_KNOTS ( 'NONE', 3,
 ( #78044, #95956, #44462, #104911, #46134, #96511 ),
 .UNSPECIFIED., .F., .F.,
 ( 4, 2, 4 ),
 ( 8.752084563234713870E-15, 0.0005716314000290802439, 0.001143262800049408374 ),
 .UNSPECIFIED. ) ;
#55565=CARTESIAN_POINT ( 'NONE',  ( 9.093835586139999094, 1363.023136422000107, 210.6218459616991936 ) ) ;
#55599=EDGE_LOOP ( 'NONE', ( #69142, #110641, #44896, #8700, #45952, #15478, #16694, #14251, #9291, #13801 ) ) ;
#55608=CARTESIAN_POINT ( 'NONE',  ( -3.160946274158207281, 1370.089580311054988, 210.3387270294440157 ) ) ;
#55617=AXIS2_PLACEMENT_3D ( 'NONE', #64754, #14852, #99405 ) ;
#55707=CARTESIAN_POINT ( 'NONE',  ( 6.018929517001535778, 1367.483508091049089, 207.6218459616988241 ) ) ;
#55838=CARTESIAN_POINT ( 'NONE',  ( 5.320869478628496907, 1362.102029591487508, 207.6218459616988241 ) ) ;
#55856=CARTESIAN_POINT ( 'NONE',  ( 8.801875223506129942, 1360.481346938555589, 208.3718459617010978 ) ) ;
#55877=CARTESIAN_POINT ( 'NONE',  ( -9.934709065799999905, 1365.494406819939968, 207.6218459616989946 ) ) ;
#55967=CARTESIAN_POINT ( 'NONE',  ( -11.09489115964376360, 1365.835216822674965, 210.6218459617030021 ) ) ;
#56101=CARTESIAN_POINT ( 'NONE',  ( 3.756023522780000068, 1369.098589419769951, 210.6218459616991936 ) ) ;
#56131=CONICAL_SURFACE ( 'NONE', #7831, 23.60271693650006952, 1.047191723200000313 ) ;
#56236=CARTESIAN_POINT ( 'NONE',  ( 3.756023522788400015, 1369.098589419797918, 210.6218459616987957 ) ) ;
#56262=CARTESIAN_POINT ( 'NONE',  ( 3.756023522790000069, 1369.098589419769951, 207.6218459616989946 ) ) ;
#56375=CARTESIAN_POINT ( 'NONE',  ( 3.426613460960000079, 1360.656565846710009, 207.6218459616989946 ) ) ;
#56391=CARTESIAN_POINT ( 'NONE',  ( 10.88871838020139826, 1364.006426590386127, 207.6218459616987673 ) ) ;
#56416=CARTESIAN_POINT ( 'NONE',  ( -8.988712649806421595, 1365.105188660967315, 207.6218459616988241 ) ) ;
#56519=CARTESIAN_POINT ( 'NONE',  ( -8.538839991170000587, 1362.569232148550100, 207.6218459616989946 ) ) ;
#56584=( BOUNDED_CURVE ( )  B_SPLINE_CURVE ( 5, ( #109191, #8907, #43084, #18399, #33005, #94019 ),
 .UNSPECIFIED., .F., .F. ) 
 B_SPLINE_CURVE_WITH_KNOTS ( ( 6, 6 ),
 ( 0.000000000000000000, 1.000000000000000000 ),
 .UNSPECIFIED. ) 
 CURVE ( )  GEOMETRIC_REPRESENTATION_ITEM ( )  RATIONAL_B_SPLINE_CURVE ( ( 1.000000000000000000, 0.8718535683296719796, 0.7642340215966414441, 0.6738533009783809202, 0.5979500389088989731, 0.5342895590787407611 ) ) 
 REPRESENTATION_ITEM ( '' )  );
#56604=CARTESIAN_POINT ( 'NONE',  ( -3.200208250563545853, 1370.366478648552174, 206.6667948705140532 ) ) ;
#56638=DIRECTION ( 'NONE',  ( 0.4794255386042021172, -2.935634756405659236E-17, -0.8775825618903732028 ) ) ;
#56651=FACE_OUTER_BOUND ( 'NONE', #64412, .T. ) ;
#56691=CARTESIAN_POINT ( 'NONE',  ( -3.088273073808346147, 1369.577046551927879, 210.5855487400704078 ) ) ;
#56790=CARTESIAN_POINT ( 'NONE',  ( 8.040263484913412029, 1366.379670611970141, 207.6218459616988241 ) ) ;
#56926=CARTESIAN_POINT ( 'NONE',  ( -5.364860563355343004, 1363.173009576943059, 209.6218459617148824 ) ) ;
#56928=B_SPLINE_CURVE_WITH_KNOTS ( 'NONE', 3,
 ( #36443, #103656, #36994, #35348, #26383, #104757 ),
 .UNSPECIFIED., .F., .F.,
 ( 4, 2, 4 ),
 ( 0.4999572393258174818, 0.7499786196629087964, 1.000000000000000000 ),
 .UNSPECIFIED. ) ;
#56945=CARTESIAN_POINT ( 'NONE',  ( 10.80894745490800624, 1367.705630506329499, 208.3718459617010978 ) ) ;
#56970=CARTESIAN_POINT ( 'NONE',  ( -8.725041378416754867, 1365.289353615551363, 210.6218459617142003 ) ) ;
#57014=DIRECTION ( 'NONE',  ( -0.8775825618903760894, 0.000000000000000000, -0.4794255386041968436 ) ) ;
#57081=CARTESIAN_POINT ( 'NONE',  ( -10.47377929740979141, 1362.785267724748564, 210.6218459617030021 ) ) ;
#57157=AXIS2_PLACEMENT_3D ( 'NONE', #107588, #22448, #1160 ) ;
#57250=ORIENTED_EDGE ( 'NONE', *, *, #57628, .T. ) ;
#57321=DIRECTION ( 'NONE',  ( 1.407418274235009893E-17, 1.000000000000000000, -2.576261870300909820E-17 ) ) ;
#57339=VECTOR ( 'NONE', #54759, 999.9999999999998863 ) ;
#57429=CARTESIAN_POINT ( 'NONE',  ( -4.404634328387945885, 1370.457478306087751, 209.4202803877028600 ) ) ;
#57454=DIRECTION ( 'NONE',  ( 3.828568698926946970E-16, 0.000000000000000000, -1.000000000000000000 ) ) ;
#57489=B_SPLINE_CURVE_WITH_KNOTS ( 'NONE', 3,
 ( #64300, #98420, #5469, #46403, #39629, #81609 ),
 .UNSPECIFIED., .F., .F.,
 ( 4, 2, 4 ),
 ( 0.000000000000000000, 0.2499786196629087409, 0.4999572393258174818 ),
 .UNSPECIFIED. ) ;
#57490=CARTESIAN_POINT ( 'NONE',  ( 8.257515364769007604, 1363.888049817303681, 210.6218459617142003 ) ) ;
#57506=CARTESIAN_POINT ( 'NONE',  ( 10.53407823797624232, 1366.566494964519279, 207.6218459616987673 ) ) ;
#57525=LINE ( 'NONE', #83800, #94564 ) ;
#57628=EDGE_CURVE ( 'NONE', #5019, #27860, #7072, .T. ) ;
#57638=CARTESIAN_POINT ( 'NONE',  ( -10.08466507605109719, 1362.620900815653613, 207.6218459616987673 ) ) ;
#57726=ADVANCED_FACE ( 'NONE', ( #38590 ), #106897, .F. ) ;
#57802=CARTESIAN_POINT ( 'NONE',  ( -2.742048936847579998, 1367.348608298013232, 208.3718459617061285 ) ) ;
#58030=CARTESIAN_POINT ( 'NONE',  ( 8.716786869081156297, 1364.517005822695410, 210.6218459617142003 ) ) ;
#58047=CARTESIAN_POINT ( 'NONE',  ( 9.813910351400000565, 1364.017814053650000, 207.6218459616989946 ) ) ;
#58147=ORIENTED_EDGE ( 'NONE', *, *, #28124, .T. ) ;
#58174=CARTESIAN_POINT ( 'NONE',  ( -8.082564370840000123, 1362.241991287400197, 207.6218459616989946 ) ) ;
#58250=EDGE_CURVE ( 'NONE', #40999, #74254, #109070, .T. ) ;
#58277=FACE_OUTER_BOUND ( 'NONE', #17633, .T. ) ;
#58361=DIRECTION ( 'NONE',  ( -6.123233995736769734E-17, -1.000000000000000000, 7.888609052210119587E-33 ) ) ;
#58450=ORIENTED_EDGE ( 'NONE', *, *, #104758, .F. ) ;
#58515=CARTESIAN_POINT ( 'NONE',  ( -3.877733327704724342, 1370.349513340957628, 208.3133770646377059 ) ) ;
#58580=CARTESIAN_POINT ( 'NONE',  ( 7.877099145829999038, 1362.118768394180051, 207.6218459616989946 ) ) ;
#58594=CARTESIAN_POINT ( 'NONE',  ( 9.813910351407720611, 1364.017814053649772, 210.6218459616991936 ) ) ;
#58618=CARTESIAN_POINT ( 'NONE',  ( 8.578717400394859958E-16, 1374.913060387289988, 209.1218459616989946 ) ) ;
#58721=CARTESIAN_POINT ( 'NONE',  ( -8.512285033948522539, 1360.184861213356498, 209.6218459617033432 ) ) ;
#58821=DIRECTION ( 'NONE',  ( 0.9900965937346507539, -0.1403878024439509931, 3.790652827686679061E-16 ) ) ;
#58835=AXIS2_PLACEMENT_3D ( 'NONE', #66510, #49144, #93319 ) ;
#58844=CARTESIAN_POINT ( 'NONE',  ( -6.393428210657781108, 1363.466147642558553, 208.3718459617061285 ) ) ;
#58878=FACE_BOUND ( 'NONE', #32114, .T. ) ;
#59140=CARTESIAN_POINT ( 'NONE',  ( 9.622136349646140729, 1363.684386430199993, 210.6218459616987957 ) ) ;
#59152=AXIS2_PLACEMENT_3D ( 'NONE', #63885, #64978, #105317 ) ;
#59156=CARTESIAN_POINT ( 'NONE',  ( 9.231361398829999843, 1366.659448741839924, 207.6218459616989946 ) ) ;
#59168=ADVANCED_FACE ( 'NONE', ( #58878, #16283 ), #84610, .F. ) ;
#59222=UNCERTAINTY_MEASURE_WITH_UNIT (LENGTH_MEASURE( 1.000000000000000082E-05 ), #43444, 'distance_accuracy_value', 'NONE');
#59290=CARTESIAN_POINT ( 'NONE',  ( -2.380813228428187767, 1360.502616939895915, 210.6218459616991936 ) ) ;
#59410=CARTESIAN_POINT ( 'NONE',  ( -8.014696367955107092, 1363.426607574581794, 207.6218459616988241 ) ) ;
#59541=CARTESIAN_POINT ( 'NONE',  ( 2.880836473691240407, 1368.383867273139913, 210.4211859087380105 ) ) ;
#59613=ORIENTED_EDGE ( 'NONE', *, *, #60704, .F. ) ;
#59665=EDGE_LOOP ( 'NONE', ( #73226, #72648, #107337, #84428, #102826 ) ) ;
#59682=CARTESIAN_POINT ( 'NONE',  ( 9.258247136799999666, 1363.198586359130104, 207.6218459616989946 ) ) ;
#59696=CARTESIAN_POINT ( 'NONE',  ( 5.528921214552624974, 1369.939580316713773, 210.6218459617030021 ) ) ;
#59758=ORIENTED_EDGE ( 'NONE', *, *, #23305, .F. ) ;
#59833=CARTESIAN_POINT ( 'NONE',  ( 3.586287380388563317, 1359.668001507771805, 207.6218459616987673 ) ) ;
#59920=CARTESIAN_POINT ( 'NONE',  ( -3.200208338885655479, 1370.366479271463049, 211.5769014320682970 ) ) ;
#59962=CARTESIAN_POINT ( 'NONE',  ( -8.251318938499840883, 1363.612701139454202, 207.6218459616988241 ) ) ;
#59970=CARTESIAN_POINT ( 'NONE',  ( -9.934214826642712381, 1367.375828905819617, 207.6218459616987673 ) ) ;
#60114=ORIENTED_EDGE ( 'NONE', *, *, #40518, .F. ) ;
#60149=ORIENTED_EDGE ( 'NONE', *, *, #17901, .T. ) ;
#60232=CARTESIAN_POINT ( 'NONE',  ( 7.999617675857605192, 1364.906918534513807, 209.6218459617148824 ) ) ;
#60249=CARTESIAN_POINT ( 'NONE',  ( 9.231361398833680454, 1366.659448741839924, 210.6218459616991936 ) ) ;
#60314=PRODUCT_DEFINITION_CONTEXT ( 'detailed design', #72126, 'design' ) ;
#60384=CARTESIAN_POINT ( 'NONE',  ( 3.426613460960000079, 1360.656565846710009, 207.6218459616989946 ) ) ;
#60412=CARTESIAN_POINT ( 'NONE',  ( -3.763781937370000108, 1369.097489338550076, 207.6218459616989946 ) ) ;
#60483=EDGE_CURVE ( 'NONE', #63480, #97580, #91919, .T. ) ;
#60506=VERTEX_POINT ( 'NONE', #99063 ) ;
#60510=CARTESIAN_POINT ( 'NONE',  ( -7.816276179476305153, 1364.594548665079628, 209.6218459617148824 ) ) ;
#60519=CARTESIAN_POINT ( 'NONE',  ( -5.551604495410622953, 1369.933960282451608, 210.6218459617030021 ) ) ;
#60619=CIRCLE ( 'NONE', #53505, 3.000000000000002665 ) ;
#60704=EDGE_CURVE ( 'NONE', #9968, #32551, #52612, .T. ) ;
#60802=CARTESIAN_POINT ( 'NONE',  ( 8.099654910236120386, 1364.797801192799852, 208.3718459617061285 ) ) ;
#60817=SURFACE_SIDE_STYLE ('',( #77048 ) ) ;
#60819=CARTESIAN_POINT ( 'NONE',  ( 8.792358245598531852, 1369.487036709539780, 209.6218459617033432 ) ) ;
#60830=CARTESIAN_POINT ( 'NONE',  ( -7.450033292399999674, 1367.931913175460068, 207.6218459616989946 ) ) ;
#60950=CARTESIAN_POINT ( 'NONE',  ( 4.466423236866957858, 1359.830825915227024, 207.6218459616987673 ) ) ;
#60976=CARTESIAN_POINT ( 'NONE',  ( -7.826724685212123056, 1365.218692947454656, 209.6218459617148824 ) ) ;
#61064=CARTESIAN_POINT ( 'NONE',  ( -2.845570814896624334, 1367.865368787501211, 208.4582261696480430 ) ) ;
#61081=CARTESIAN_POINT ( 'NONE',  ( -7.040068640382609821, 1363.032232768721542, 210.6218459617142003 ) ) ;
#61089=CARTESIAN_POINT ( 'NONE',  ( -4.736400914510313420, 1369.930404928426242, 207.6218459616987673 ) ) ;
#61151=DIRECTION ( 'NONE',  ( 3.828568698926946970E-16, 0.000000000000000000, -1.000000000000000000 ) ) ;
#61165=TOROIDAL_SURFACE ( 'NONE', #34351, 9.500000000000000000, 0.5000000000000000000 ) ;
#61288=PLANE ( 'NONE',  #66374 ) ;
#61360=CARTESIAN_POINT ( 'NONE',  ( 8.635439922379047673, 1365.453094710691630, 210.6218459617142003 ) ) ;
#61373=CARTESIAN_POINT ( 'NONE',  ( 7.890486628608978315, 1368.832605670318799, 207.6218459616987673 ) ) ;
#61383=CARTESIAN_POINT ( 'NONE',  ( -9.655745333040000489, 1363.739547551590022, 207.6218459616989946 ) ) ;
#61496=CARTESIAN_POINT ( 'NONE',  ( -4.745098151869999725, 1360.923919868640041, 207.6218459616989946 ) ) ;
#61524=CARTESIAN_POINT ( 'NONE',  ( -8.696701630039340714, 1367.135748871443866, 210.6218459616987957 ) ) ;
#61613=CARTESIAN_POINT ( 'NONE',  ( 6.161840689439245899, 1363.362512618330584, 208.3718459617061285 ) ) ;
#61622=CARTESIAN_POINT ( 'NONE',  ( -9.938521104460262379, 1368.703998991882372, 209.6218459617033432 ) ) ;
#61650=ORIENTED_EDGE ( 'NONE', *, *, #43488, .F. ) ;
#61769=CARTESIAN_POINT ( 'NONE',  ( -9.832966357650001044, 1364.062280235949856, 210.6218459616991936 ) ) ;
#61909=CARTESIAN_POINT ( 'NONE',  ( 9.925983360928359645, 1364.303202023261974, 210.6218459616987957 ) ) ;
#61937=CARTESIAN_POINT ( 'NONE',  ( -10.02185219039999886, 1364.916310432309956, 207.6218459616989946 ) ) ;
#62055=CARTESIAN_POINT ( 'NONE',  ( 10.46820095950955398, 1363.150210183547188, 207.6218459616987673 ) ) ;
#62081=CARTESIAN_POINT ( 'NONE',  ( -6.838394287845894759, 1365.988278472367028, 209.6218459617148824 ) ) ;
#62082=ORIENTED_EDGE ( 'NONE', *, *, #28769, .F. ) ;
#62174=CARTESIAN_POINT ( 'NONE',  ( -2.273521285762763355, 1361.498772813854885, 207.6218459616988241 ) ) ;
#62182=CARTESIAN_POINT ( 'NONE',  ( -6.371134682375720892, 1368.423166410909971, 210.6218459616991936 ) ) ;
#62211=AXIS2_PLACEMENT_3D ( 'NONE', #74530, #63934, #4024 ) ;
#62327=CARTESIAN_POINT ( 'NONE',  ( -9.178315062059999363, 1363.109187794150102, 210.6218459616991936 ) ) ;
#62357=ORIENTED_EDGE ( 'NONE', *, *, #60704, .T. ) ;
#62367=CARTESIAN_POINT ( 'NONE',  ( 2.561957929796739641, 1389.413060387289988, 207.5609578920601450 ) ) ;
#62439=CIRCLE ( 'NONE', #15932, 3.500000000000003109 ) ;
#62469=CARTESIAN_POINT ( 'NONE',  ( 9.842969107809999230, 1365.740588703660023, 207.6218459616989946 ) ) ;
#62495=CARTESIAN_POINT ( 'NONE',  ( 9.943976501839999926, 1365.461622992600041, 207.6218459616989946 ) ) ;
#62625=CARTESIAN_POINT ( 'NONE',  ( 9.989381280457715562, 1361.309659810096264, 208.3718459617010978 ) ) ;
#62646=CARTESIAN_POINT ( 'NONE',  ( -7.951609945375088806, 1366.194798799167529, 210.6218459617142003 ) ) ;
#62751=CARTESIAN_POINT ( 'NONE',  ( -9.977700672452339603, 1365.292605733889786, 210.6218459616991936 ) ) ;
#62807=DIRECTION ( 'NONE',  ( 0.8775825618903763115, 0.000000000000000000, 0.4794255386041965106 ) ) ;
#62901=CARTESIAN_POINT ( 'NONE',  ( -8.962252599310000178, 1366.920250605820002, 210.6218459616991936 ) ) ;
#63030=CARTESIAN_POINT ( 'NONE',  ( 4.692298114210420756, 1366.846184049853036, 209.6218459617148824 ) ) ;
#63044=CARTESIAN_POINT ( 'NONE',  ( 3.145663868875199221, 1370.195136005008180, 207.6218459616987673 ) ) ;
#63054=CARTESIAN_POINT ( 'NONE',  ( -9.178315062050000250, 1363.109187794150102, 207.6218459616989946 ) ) ;
#63074=DIRECTION ( 'NONE',  ( -0.8775825618903703162, 0.000000000000000000, -0.4794255386042076128 ) ) ;
#63172=CARTESIAN_POINT ( 'NONE',  ( 9.454737631249999552, 1363.431170718789872, 207.6218459616989946 ) ) ;
#63194=CARTESIAN_POINT ( 'NONE',  ( -8.962252599310001955, 1366.920250605820002, 207.6218459616989946 ) ) ;
#63289=CARTESIAN_POINT ( 'NONE',  ( -10.02185219039999886, 1364.916310432309956, 207.6218459616989946 ) ) ;
#63358=CARTESIAN_POINT ( 'NONE',  ( -1.331958139231829923E-15, 1375.413060387289988, 209.1218459616989946 ) ) ;
#63373=CARTESIAN_POINT ( 'NONE',  ( 4.234273392930074209, 1370.421192169647384, 208.5750769448261224 ) ) ;
#63480=VERTEX_POINT ( 'NONE', #67165 ) ;
#63565=CARTESIAN_POINT ( 'NONE',  ( 6.556794880282631688, 1366.140135904955741, 209.6218459617148824 ) ) ;
#63578=FACE_OUTER_BOUND ( 'NONE', #5964, .T. ) ;
#63580=CARTESIAN_POINT ( 'NONE',  ( 3.969839694839903288, 1370.280274951255933, 210.6218459617030021 ) ) ;
#63609=CARTESIAN_POINT ( 'NONE',  ( -7.020660495122976741, 1374.031200045389824, 205.2864416528653635 ) ) ;
#63660=CARTESIAN_POINT ( 'NONE',  ( 8.775825618903722258, 1374.413060387289988, 213.9161013477410336 ) ) ;
#63710=CARTESIAN_POINT ( 'NONE',  ( 8.796059898609998484, 1362.759824263850078, 207.6218459616989946 ) ) ;
#63730=CARTESIAN_POINT ( 'NONE',  ( -8.799096642483785757, 1365.569276427433351, 207.6218459616988241 ) ) ;
#63757=EDGE_CURVE ( 'NONE', #69033, #53641, #21677, .T. ) ;
#63829=CARTESIAN_POINT ( 'NONE',  ( -11.83205321494600781, 1365.644012745619875, 208.3718459617010978 ) ) ;
#63860=AXIS2_PLACEMENT_3D ( 'NONE', #49957, #58361, #77366 ) ;
#63874=EDGE_LOOP ( 'NONE', ( #87936, #78618, #47530, #68919 ) ) ;
#63879=CIRCLE ( 'NONE', #40596, 2.000000000000004441 ) ;
#63885=CARTESIAN_POINT ( 'NONE',  ( -9.724834716106559089E-16, 1374.031200045389824, 209.1218459616989946 ) ) ;
#63923=EDGE_CURVE ( 'NONE', #66318, #3293, #94141, .T. ) ;
#63934=DIRECTION ( 'NONE',  ( -6.123233995736769734E-17, -1.000000000000000000, 0.000000000000000000 ) ) ;
#63936=CARTESIAN_POINT ( 'NONE',  ( -0.9985884068039365680, 1368.656381781917617, 207.8228078564805230 ) ) ;
#63974=CARTESIAN_POINT ( 'NONE',  ( 8.379275254589998667, 1362.454991452510058, 210.6218459616991936 ) ) ;
#63983=ORIENTED_EDGE ( 'NONE', *, *, #40518, .T. ) ;
#64104=CARTESIAN_POINT ( 'NONE',  ( 7.233739725823942202, 1366.686151722334898, 210.6218459617142003 ) ) ;
#64220=ORIENTED_EDGE ( 'NONE', *, *, #73258, .T. ) ;
#64238=CARTESIAN_POINT ( 'NONE',  ( 1.655301970317450966, 1361.639372583430031, 210.6218459617142003 ) ) ;
#64253=CARTESIAN_POINT ( 'NONE',  ( 9.258247136799999666, 1363.198586359130104, 207.6218459616989946 ) ) ;
#64278=CARTESIAN_POINT ( 'NONE',  ( -7.988138845717701386, 1364.969037029785568, 209.6218459617148824 ) ) ;
#64298=ORIENTED_EDGE ( 'NONE', *, *, #104366, .T. ) ;
#64300=CARTESIAN_POINT ( 'NONE',  ( -2.919081270098979441, 1368.383855509380055, 210.4211783971049954 ) ) ;
#64375=CARTESIAN_POINT ( 'NONE',  ( -10.73381386015609174, 1366.619851243301127, 210.6218459617030021 ) ) ;
#64376=DIRECTION ( 'NONE',  ( 0.000000000000000000, 2.700129756073435379E-15, -1.000000000000000000 ) ) ;
#64384=B_SPLINE_CURVE_WITH_KNOTS ( 'NONE', 3,
 ( #59541, #8561, #42733, #102602 ),
 .UNSPECIFIED., .F., .F.,
 ( 4, 4 ),
 ( 0.000000000000000000, 1.000000000000000000 ),
 .UNSPECIFIED. ) ;
#64412=EDGE_LOOP ( 'NONE', ( #78591, #20661, #12749, #99850 ) ) ;
#64521=CARTESIAN_POINT ( 'NONE',  ( -7.173827098680000347, 1361.757975858879945, 210.6218459616991936 ) ) ;
#64658=CARTESIAN_POINT ( 'NONE',  ( 4.092070562564425806, 1367.124094438674774, 208.3718459617061285 ) ) ;
#64727=AXIS2_PLACEMENT_3D ( 'NONE', #430, #8229, #42396 ) ;
#64754=CARTESIAN_POINT ( 'NONE',  ( -3.061616997868380553E-17, 1389.413060387289988, 209.1218459616989946 ) ) ;
#64760=ORIENTED_EDGE ( 'NONE', *, *, #109804, .T. ) ;
#64797=CARTESIAN_POINT ( 'NONE',  ( 3.266939541527484003, 1361.645130185650032, 207.6218459616988241 ) ) ;
#64815=CARTESIAN_POINT ( 'NONE',  ( 11.69568758614039083, 1366.517700528763953, 209.6218459617033432 ) ) ;
#64836=CARTESIAN_POINT ( 'NONE',  ( -8.967890654244879300, 1365.210398484327470, 207.6218459616988241 ) ) ;
#64838=ORIENTED_EDGE ( 'NONE', *, *, #58250, .F. ) ;
#64926=CARTESIAN_POINT ( 'NONE',  ( -10.73667021122307297, 1363.210612206614996, 210.6218459617030021 ) ) ;
#64961=ADVANCED_FACE ( 'NONE', ( #74805 ), #56131, .F. ) ;
#64969=ORIENTED_EDGE ( 'NONE', *, *, #18113, .F. ) ;
#64978=DIRECTION ( 'NONE',  ( 1.407418274235009893E-17, 1.000000000000000000, -2.576261870300909820E-17 ) ) ;
#65060=CARTESIAN_POINT ( 'NONE',  ( 9.369782510120000296, 1366.497526915279877, 210.6218459616991936 ) ) ;
#65071=CARTESIAN_POINT ( 'NONE',  ( 2.632747685671115612, 1379.913060387289988, 210.5601225775116063 ) ) ;
#65091=AXIS2_PLACEMENT_3D ( 'NONE', #7903, #42074, #25239 ) ;
#65199=CARTESIAN_POINT ( 'NONE',  ( 7.001358796384309358, 1367.037625826739713, 207.6218459616988241 ) ) ;
#65338=CARTESIAN_POINT ( 'NONE',  ( 3.127224862021169560, 1362.510123982220193, 208.3718459617061285 ) ) ;
#65355=CARTESIAN_POINT ( 'NONE',  ( 10.70668172122111095, 1366.667713169411172, 210.6218459617030021 ) ) ;
#65380=CARTESIAN_POINT ( 'NONE',  ( -8.726294317499757369, 1364.539843072939220, 210.6218459617142003 ) ) ;
#65480=CARTESIAN_POINT ( 'NONE',  ( -10.51336953340124758, 1363.224273292747284, 207.6218459616987673 ) ) ;
#65646=LINE ( 'NONE', #100331, #85225 ) ;
#65695=CIRCLE ( 'NONE', #92429, 18.16666666670000296 ) ;
#65818=CARTESIAN_POINT ( 'NONE',  ( -3.743571413909633439, 1370.323971799861056, 208.2444943395997825 ) ) ;
#65885=CARTESIAN_POINT ( 'NONE',  ( 8.796059898617141215, 1362.759824263836208, 210.6218459616987957 ) ) ;
#65903=CARTESIAN_POINT ( 'NONE',  ( 10.75464559463706671, 1366.583021909888885, 210.6218459617030021 ) ) ;
#65922=ADVANCED_FACE ( 'NONE', ( #108138 ), #34015, .T. ) ;
#65929=CARTESIAN_POINT ( 'NONE',  ( -9.832966357650001044, 1364.062280235949856, 207.6218459616989946 ) ) ;
#65993=MECHANICAL_DESIGN_GEOMETRIC_PRESENTATION_REPRESENTATION('',(#99919),#83860);
#66036=CARTESIAN_POINT ( 'NONE',  ( -9.701269302676793771, 1361.953484705324172, 210.6218459617030021 ) ) ;
#66176=CARTESIAN_POINT ( 'NONE',  ( -3.005276066430516035, 1369.205039411270036, 210.6218459616991936 ) ) ;
#66177=CARTESIAN_POINT ( 'NONE',  ( 9.984115569229999210, 1365.258395869460173, 210.6218459616991936 ) ) ;
#66318=VERTEX_POINT ( 'NONE', #59920 ) ;
#66374=AXIS2_PLACEMENT_3D ( 'NONE', #78603, #45028, #12498 ) ;
#66380=CARTESIAN_POINT ( 'NONE',  ( -4.118752830811812871, 1370.397247303622407, 209.7672875607871958 ) ) ;
#66443=CARTESIAN_POINT ( 'NONE',  ( 8.476942927299997876, 1362.523913559720086, 207.6218459616989946 ) ) ;
#66449=EDGE_CURVE ( 'NONE', #101372, #36895, #38370, .T. ) ;
#66464=CARTESIAN_POINT ( 'NONE',  ( 9.704582620010000937, 1366.001145740639913, 207.6218459616989946 ) ) ;
#66510=CARTESIAN_POINT ( 'NONE',  ( -9.724834716106559089E-16, 1374.031200045389824, 209.1218459616989946 ) ) ;
#66592=CARTESIAN_POINT ( 'NONE',  ( -10.56256883942626068, 1363.309231799455802, 207.6218459616987673 ) ) ;
#66691=DIRECTION ( 'NONE',  ( -6.123233995736769734E-17, -1.000000000000000000, 0.000000000000000000 ) ) ;
#66720=CARTESIAN_POINT ( 'NONE',  ( -3.942352636383586795, 1370.082171903791277, 207.6218459616987673 ) ) ;
#66743=SHAPE_DEFINITION_REPRESENTATION ( #36561, #83713 ) ;
#66985=CARTESIAN_POINT ( 'NONE',  ( 6.892224678239999847, 1361.632554499750086, 207.6218459616989946 ) ) ;
#67003=CARTESIAN_POINT ( 'NONE',  ( 11.06163309507687664, 1367.380938442054003, 208.3718459617010978 ) ) ;
#67135=CARTESIAN_POINT ( 'NONE',  ( -10.31239467132616561, 1362.904424737038880, 207.6218459616987673 ) ) ;
#67165=CARTESIAN_POINT ( 'NONE',  ( 3.160865718646527434, 1370.358796302880364, 211.5724212009420739 ) ) ;
#67438=EDGE_LOOP ( 'NONE', ( #107843, #50618, #12814, #1549 ) ) ;
#67541=CARTESIAN_POINT ( 'NONE',  ( 8.379275254603339107, 1362.454991452494141, 210.6218459616987957 ) ) ;
#67553=( NAMED_UNIT ( * ) PLANE_ANGLE_UNIT ( ) SI_UNIT ( $, .RADIAN. ) );
#67555=CARTESIAN_POINT ( 'NONE',  ( 5.215187551879999717, 1368.779556716650177, 207.6218459616989946 ) ) ;
#67688=CARTESIAN_POINT ( 'NONE',  ( -5.986709854327127545, 1361.264879806976069, 210.6218459616991936 ) ) ;
#67716=AXIS2_PLACEMENT_3D ( 'NONE', #48409, #6932, #23727 ) ;
#67776=AXIS2_PLACEMENT_3D ( 'NONE', #43021, #49770, #34052 ) ;
#67806=CARTESIAN_POINT ( 'NONE',  ( -7.940496932319466517, 1364.770096069278225, 209.6218459617148824 ) ) ;
#68098=CARTESIAN_POINT ( 'NONE',  ( 7.811382534051993787, 1363.278400952723359, 207.6218459616988241 ) ) ;
#68112=( NAMED_UNIT ( * ) SI_UNIT ( $, .STERADIAN. ) SOLID_ANGLE_UNIT ( ) );
#68114=CARTESIAN_POINT ( 'NONE',  ( 4.763849656990267079, 1370.128942875427583, 210.6218459617030021 ) ) ;
#68184=UNCERTAINTY_MEASURE_WITH_UNIT (LENGTH_MEASURE( 1.000000000000000082E-05 ), #2320, 'distance_accuracy_value', 'NONE');
#68251=CARTESIAN_POINT ( 'NONE',  ( 5.887860814122072739, 1360.176812065337344, 207.6218459616987673 ) ) ;
#68366=CARTESIAN_POINT ( 'NONE',  ( -9.328535443860001664, 1363.278783432130012, 207.6218459616989946 ) ) ;
#68374=CARTESIAN_POINT ( 'NONE',  ( -10.30220861077111216, 1368.409031475352094, 209.6218459617033432 ) ) ;
#68445=VERTEX_POINT ( 'NONE', #12423 ) ;
#68457=CARTESIAN_POINT ( 'NONE',  ( -2.813822098188480059, 1367.641464703512383, 209.1220808600859300 ) ) ;
#68594=DIRECTION ( 'NONE',  ( -1.407418274235009893E-17, -1.000000000000000000, 2.576261870300909820E-17 ) ) ;
#68644=CARTESIAN_POINT ( 'NONE',  ( 8.991947938729746070, 1365.087450627709131, 207.6218459616988241 ) ) ;
#68658=CARTESIAN_POINT ( 'NONE',  ( 9.901269661657691401, 1368.573894001910048, 208.3718459617010978 ) ) ;
#68770=AXIS2_PLACEMENT_3D ( 'NONE', #94968, #18237, #50224 ) ;
#68797=CARTESIAN_POINT ( 'NONE',  ( 4.507237278552312709, 1359.634735991508478, 210.6218459617030021 ) ) ;
#68822=CARTESIAN_POINT ( 'NONE',  ( -3.549497098556182006, 1367.915870260280144, 210.6218459617142003 ) ) ;
#68919=ORIENTED_EDGE ( 'NONE', *, *, #48439, .F. ) ;
#68922=CARTESIAN_POINT ( 'NONE',  ( -8.047699957360343603, 1364.705686786927117, 208.3718459617061285 ) ) ;
#68930=CARTESIAN_POINT ( 'NONE',  ( -4.928286345013006553, 1370.785306328871684, 208.3718459617010978 ) ) ;
#68983=CARTESIAN_POINT ( 'NONE',  ( -3.125914921230999788, 1369.842518795720025, 211.2713650144889925 ) ) ;
#69028=EDGE_CURVE ( 'NONE', #7609, #53641, #12364, .T. ) ;
#69033=VERTEX_POINT ( 'NONE', #76064 ) ;
#69102=PRODUCT_DEFINITION_FORMATION_WITH_SPECIFIED_SOURCE ( 'ANY', '', #54500, .NOT_KNOWN. ) ;
#69142=ORIENTED_EDGE ( 'NONE', *, *, #29916, .T. ) ;
#69192=CARTESIAN_POINT ( 'NONE',  ( 8.972728618379855803, 1365.192543519359333, 207.6218459616988241 ) ) ;
#69206=CARTESIAN_POINT ( 'NONE',  ( 9.979564351426096991, 1368.671368999377137, 209.6218459617033432 ) ) ;
#69216=CARTESIAN_POINT ( 'NONE',  ( -3.787329988085039734, 1369.092969256092601, 207.6218459616989946 ) ) ;
#69217=CIRCLE ( 'NONE', #29866, 17.26401014167801762 ) ;
#69270=ORIENTED_EDGE ( 'NONE', *, *, #36956, .T. ) ;
#69345=CARTESIAN_POINT ( 'NONE',  ( -5.986709854369999917, 1361.264879806939916, 207.6218459616989946 ) ) ;
#69354=TOROIDAL_SURFACE ( 'NONE', #1397, 8.000000000000000000, 2.000000000000000000 ) ;
#69374=CARTESIAN_POINT ( 'NONE',  ( -9.351945459745801159, 1366.519103298168147, 210.6218459616987957 ) ) ;
#69417=CIRCLE ( 'NONE', #106937, 1.500287545630077490 ) ;
#69454=CARTESIAN_POINT ( 'NONE',  ( -2.967054383202428536, 1368.722141705661670, 210.5451987844712107 ) ) ;
#69471=CARTESIAN_POINT ( 'NONE',  ( -8.082564370840000123, 1362.241991287400197, 207.6218459616989946 ) ) ;
#69479=CARTESIAN_POINT ( 'NONE',  ( -9.351945459739999578, 1366.519103298159735, 207.6218459616989946 ) ) ;
#69542=CARTESIAN_POINT ( 'NONE',  ( -1.331958139231829923E-15, 1375.413060387289988, 209.1218459616989946 ) ) ;
#69621=CARTESIAN_POINT ( 'NONE',  ( -7.450033292409999675, 1367.931913175459840, 210.6218459616991936 ) ) ;
#69734=DIRECTION ( 'NONE',  ( 0.1403901404440096035, 0.9900962622220685905, 0.000000000000000000 ) ) ;
#69735=VECTOR ( 'NONE', #103953, 1000.000000000000000 ) ;
#69759=CARTESIAN_POINT ( 'NONE',  ( 9.704582620010000937, 1366.001145740639913, 207.6218459616989946 ) ) ;
#69771=FILL_AREA_STYLE ('',( #26621 ) ) ;
#69773=CARTESIAN_POINT ( 'NONE',  ( 9.271894271600004345, 1369.053083489915252, 208.3718459617010978 ) ) ;
#69783=CARTESIAN_POINT ( 'NONE',  ( -9.977700672470000143, 1365.292605733890014, 207.6218459616989946 ) ) ;
#69906=CARTESIAN_POINT ( 'NONE',  ( -7.173827098674079750, 1361.757975858879945, 210.6218459616991936 ) ) ;
#69933=CARTESIAN_POINT ( 'NONE',  ( -8.232155009519999567, 1367.485244382299925, 207.6218459616989946 ) ) ;
#70014=CARTESIAN_POINT ( 'NONE',  ( -2.850903925664035832, 1367.902980992500716, 209.8767901781862690 ) ) ;
#70033=CARTESIAN_POINT ( 'NONE',  ( -7.674634134560755605, 1364.272616766665806, 208.3718459617061285 ) ) ;
#70041=CARTESIAN_POINT ( 'NONE',  ( -4.120923335396738274, 1371.066854469031114, 209.6218459617033432 ) ) ;
#70098=CARTESIAN_POINT ( 'NONE',  ( -1.122592899216370017E-16, 1388.079727053959914, 209.1218459616989946 ) ) ;
#70126=CARTESIAN_POINT ( 'NONE',  ( 4.456500632703686016, 1370.468720332280100, 209.2823377659277924 ) ) ;
#70286=ORIENTED_EDGE ( 'NONE', *, *, #58250, .T. ) ;
#70317=CARTESIAN_POINT ( 'NONE',  ( 8.120855199716963568, 1364.859655959927750, 208.3718459617061285 ) ) ;
#70341=CARTESIAN_POINT ( 'NONE',  ( -3.034926079678273325, 1369.200812461397618, 207.6218459616989946 ) ) ;
#70405=ORIENTED_EDGE ( 'NONE', *, *, #36890, .T. ) ;
#70458=CARTESIAN_POINT ( 'NONE',  ( 9.060746519232587559, 1361.466900052261508, 210.6218459617030021 ) ) ;
#70485=CARTESIAN_POINT ( 'NONE',  ( -7.324900043384086956, 1366.863774163400876, 207.6218459616988241 ) ) ;
#70562=CARTESIAN_POINT ( 'NONE',  ( -3.034926079678273325, 1369.200812461397618, 207.6218459616989946 ) ) ;
#70577=CARTESIAN_POINT ( 'NONE',  ( -5.403726144051158364, 1363.053751466317181, 208.3718459617061285 ) ) ;
#70585=CARTESIAN_POINT ( 'NONE',  ( -6.711617847637158185, 1369.367247958655753, 207.6218459616987673 ) ) ;
#70736=CARTESIAN_POINT ( 'NONE',  ( -9.328535443860001664, 1363.278783432129785, 210.6218459616991936 ) ) ;
#70871=CARTESIAN_POINT ( 'NONE',  ( 9.532517564019999057, 1366.286862064870093, 207.6218459616989946 ) ) ;
#70896=CARTESIAN_POINT ( 'NONE',  ( 1.748848150589999983, 1360.440694539920059, 207.6218459616989946 ) ) ;
#71015=CARTESIAN_POINT ( 'NONE',  ( 8.205855632998520832, 1360.030193506661362, 209.6218459617033432 ) ) ;
#71039=CARTESIAN_POINT ( 'NONE',  ( -7.532495872739816356, 1365.665514383497566, 208.3718459617061285 ) ) ;
#71138=CARTESIAN_POINT ( 'NONE',  ( -11.91708563375230767, 1364.919342642561787, 208.3718459617010978 ) ) ;
#71268=CARTESIAN_POINT ( 'NONE',  ( -3.200208250563545853, 1370.366478648552174, 206.6667948705140532 ) ) ;
#71274=ADVANCED_FACE ( 'NONE', ( #30874 ), #5126, .T. ) ;
#71355=CIRCLE ( 'NONE', #101641, 10.00000000000000888 ) ;
#71430=CARTESIAN_POINT ( 'NONE',  ( 4.901453889304693057, 1367.619533116579305, 210.6218459617142003 ) ) ;
#71457=CARTESIAN_POINT ( 'NONE',  ( -8.624710350820000926, 1367.191948709370081, 207.6218459616989946 ) ) ;
#71580=CARTESIAN_POINT ( 'NONE',  ( 7.340269731167739842, 1361.836778001496214, 210.6218459616991936 ) ) ;
#71604=CARTESIAN_POINT ( 'NONE',  ( -5.732728747552154225, 1366.653013508871254, 208.3718459617061285 ) ) ;
#71707=CARTESIAN_POINT ( 'NONE',  ( -9.934709065799999905, 1365.494406819939968, 207.6218459616989946 ) ) ;
#71974=CARTESIAN_POINT ( 'NONE',  ( 3.421935753948512016, 1367.252205776827850, 208.3718459617061285 ) ) ;
#72118=CARTESIAN_POINT ( 'NONE',  ( 9.559785582989375641, 1361.831719013449856, 210.6218459617030021 ) ) ;
#72126=APPLICATION_CONTEXT ( 'automotive_design' ) ;
#72140=CARTESIAN_POINT ( 'NONE',  ( -9.934709065808439377, 1365.494406819946107, 210.6218459616987957 ) ) ;
#72232=CARTESIAN_POINT ( 'NONE',  ( -10.93574897646141153, 1366.250303372820781, 210.6218459617030021 ) ) ;
#72308=CARTESIAN_POINT ( 'NONE',  ( 4.472031081881574721, 1370.472125110218485, 209.2051454052445081 ) ) ;
#72369=CARTESIAN_POINT ( 'NONE',  ( -8.082564370840001899, 1362.241991287399969, 210.6218459616991936 ) ) ;
#72416=ORIENTED_EDGE ( 'NONE', *, *, #53835, .F. ) ;
#72495=CARTESIAN_POINT ( 'NONE',  ( 7.162147128334975577, 1365.790004795873074, 209.6218459617148824 ) ) ;
#72624=CARTESIAN_POINT ( 'NONE',  ( 0.05823133897714560109, 1360.390585217530088, 210.6218459616987957 ) ) ;
#72646=CARTESIAN_POINT ( 'NONE',  ( 9.176918871551549728, 1361.548833878397545, 210.6218459617030021 ) ) ;
#72648=ORIENTED_EDGE ( 'NONE', *, *, #41059, .T. ) ;
#72662=EDGE_CURVE ( 'NONE', #77151, #18150, #17851, .T. ) ;
#72668=CARTESIAN_POINT ( 'NONE',  ( -9.690020260125340457, 1366.026910387859971, 210.6218459616987957 ) ) ;
#72748=DIRECTION ( 'NONE',  ( -6.123233995736769734E-17, -1.000000000000000000, 7.888609052210119587E-33 ) ) ;
#72768=CARTESIAN_POINT ( 'NONE',  ( -10.93963839782591663, 1363.584717398963221, 210.6218459617030021 ) ) ;
#72803=AXIS2_PLACEMENT_3D ( 'NONE', #98551, #22370, #4515 ) ;
#72906=CARTESIAN_POINT ( 'NONE',  ( -2.380813228429999651, 1360.502616939890004, 210.6218459616991936 ) ) ;
#72944=CARTESIAN_POINT ( 'NONE',  ( -3.061914603009583402, 1369.391151255473005, 210.6218459616997336 ) ) ;
#73040=CARTESIAN_POINT ( 'NONE',  ( 4.501691961677919629, 1368.956319095248091, 210.6218459616987957 ) ) ;
#73110=CARTESIAN_POINT ( 'NONE',  ( 2.134964941497458302, 1389.913060387289988, 207.8211059036665063 ) ) ;
#73115=ORIENTED_EDGE ( 'NONE', *, *, #54917, .F. ) ;
#73171=CARTESIAN_POINT ( 'NONE',  ( -2.380813228419999650, 1360.502616939890004, 207.6218459616989946 ) ) ;
#73186=CARTESIAN_POINT ( 'NONE',  ( 11.23464237080011863, 1364.859423985571993, 210.6218459617030021 ) ) ;
#73210=CARTESIAN_POINT ( 'NONE',  ( -8.123413751219246137, 1364.885445916480421, 208.3718459617061285 ) ) ;
#73226=ORIENTED_EDGE ( 'NONE', *, *, #27140, .F. ) ;
#73258=EDGE_CURVE ( 'NONE', #96281, #53641, #107392, .T. ) ;
#73292=ADVANCED_FACE ( 'NONE', ( #89057 ), #39386, .T. ) ;
#73313=CARTESIAN_POINT ( 'NONE',  ( -9.690020260109999839, 1366.026910387849966, 207.6218459616989946 ) ) ;
#73448=CARTESIAN_POINT ( 'NONE',  ( 3.069076556224334063, 1369.654997644983041, 210.5785052009047433 ) ) ;
#73536=CARTESIAN_POINT ( 'NONE',  ( -1.078902958008049989E-15, 1372.293237941190000, 209.1218459616989946 ) ) ;
#73562=AXIS2_PLACEMENT_3D ( 'NONE', #63609, #36175, #63074 ) ;
#73605=CARTESIAN_POINT ( 'NONE',  ( 6.904968631809683011, 1366.095340045324292, 208.3718459617061285 ) ) ;
#73671=ADVANCED_FACE ( 'NONE', ( #63578 ), #78, .T. ) ;
#73738=CARTESIAN_POINT ( 'NONE',  ( 6.892224678239939450, 1361.632554499738035, 210.6218459616987957 ) ) ;
#73754=CARTESIAN_POINT ( 'NONE',  ( 9.971295257834839276, 1364.502667329742053, 210.6218459616991936 ) ) ;
#73776=CARTESIAN_POINT ( 'NONE',  ( -7.999724627149254808, 1364.917771588045298, 209.6218459617148824 ) ) ;
#73782=CARTESIAN_POINT ( 'NONE',  ( 2.742048936850008722, 1367.348608298013232, 208.3718459617061569 ) ) ;
#73824=CARTESIAN_POINT ( 'NONE',  ( -2.919081270098979441, 1368.383855509380055, 210.4211783971049954 ) ) ;
#73871=CARTESIAN_POINT ( 'NONE',  ( -9.505471540885778836, 1363.500209798504102, 210.6218459616991936 ) ) ;
#73934=FACE_OUTER_BOUND ( 'NONE', #9706, .T. ) ;
#74182=CARTESIAN_POINT ( 'NONE',  ( 8.653423937779999520, 1367.169888897630017, 207.6218459616989946 ) ) ;
#74254=VERTEX_POINT ( 'NONE', #94226 ) ;
#74288=CARTESIAN_POINT ( 'NONE',  ( 8.663307226700800001, 1364.047708251303447, 207.6218459616988241 ) ) ;
#74306=CARTESIAN_POINT ( 'NONE',  ( 10.02176186326848040, 1364.879735892741792, 210.6218459616991936 ) ) ;
#74332=CARTESIAN_POINT ( 'NONE',  ( -7.950364260026115737, 1365.038675628758710, 209.6218459617148824 ) ) ;
#74338=CARTESIAN_POINT ( 'NONE',  ( 2.864888263988467632, 1368.214942817531437, 207.6218459616987957 ) ) ;
#74433=CARTESIAN_POINT ( 'NONE',  ( -8.622403150219998480, 1362.632156860360055, 207.6218459616989946 ) ) ;
#74455=VERTEX_POINT ( 'NONE', #12843 ) ;
#74459=CARTESIAN_POINT ( 'NONE',  ( -3.180365954810094209, 1370.226539215819685, 208.0370721656823321 ) ) ;
#74530=CARTESIAN_POINT ( 'NONE',  ( -6.123233995736771213E-16, 1379.913060387289988, 209.1218459616989946 ) ) ;
#74533=CARTESIAN_POINT ( 'NONE',  ( 5.561733859871847763, 1387.291117539184825, 209.1218459616989946 ) ) ;
#74562=CARTESIAN_POINT ( 'NONE',  ( 9.842969107810001006, 1365.740588703660023, 210.6218459616991936 ) ) ;
#74591=CARTESIAN_POINT ( 'NONE',  ( -2.680760545863249966, 1370.258219039080814, 211.4729122695361241 ) ) ;
#74605=( BOUNDED_CURVE ( )  B_SPLINE_CURVE ( 5, ( #39036, #40155, #13279, #73782, #74338, #47470 ),
 .UNSPECIFIED., .F., .T. ) 
 B_SPLINE_CURVE_WITH_KNOTS ( ( 6, 6 ),
 ( 0.000000000000000000, 1.000000000000000000 ),
 .UNSPECIFIED. ) 
 CURVE ( )  GEOMETRIC_REPRESENTATION_ITEM ( )  RATIONAL_B_SPLINE_CURVE ( ( 0.2500000000000000000, 0.2499999999993640087, 0.2999999999990460298, 0.3999999999987279842, 0.5999999999987279953, 1.000000000000000000 ) ) 
 REPRESENTATION_ITEM ( '' )  );
#74686=VERTEX_POINT ( 'NONE', #107335 ) ;
#74805=FACE_OUTER_BOUND ( 'NONE', #49838, .T. ) ;
#74823=AXIS2_PLACEMENT_3D ( 'NONE', #21040, #12111, #12668 ) ;
#74833=CARTESIAN_POINT ( 'NONE',  ( 6.952323068159633301, 1363.756189849812017, 208.3718459617061285 ) ) ;
#74850=CARTESIAN_POINT ( 'NONE',  ( 10.91103383375193481, 1363.518622284593221, 210.6218459617030021 ) ) ;
#74982=CARTESIAN_POINT ( 'NONE',  ( -9.351651288933469530, 1361.678816003299744, 210.6218459617030021 ) ) ;
#75256=CARTESIAN_POINT ( 'NONE',  ( 2.742048936847579998, 1367.348608298013232, 208.3718459617061285 ) ) ;
#75388=CARTESIAN_POINT ( 'NONE',  ( 8.476942927312379084, 1362.523913559699849, 210.6218459616987957 ) ) ;
#75405=CARTESIAN_POINT ( 'NONE',  ( 10.95713404883475306, 1364.300541727352993, 207.6218459616987673 ) ) ;
#75534=CARTESIAN_POINT ( 'NONE',  ( -7.592149787980000397, 1361.964468435470053, 207.6218459616989946 ) ) ;
#75588=CARTESIAN_POINT ( 'NONE',  ( -3.187940576023601924, 1370.279959858722350, 207.3802660875432480 ) ) ;
#75764=CARTESIAN_POINT ( 'NONE',  ( 2.632747685671115168, 1375.413060387289988, 210.5601225775116063 ) ) ;
#75860=CARTESIAN_POINT ( 'NONE',  ( -1.122592899216370017E-16, 1388.079727053959914, 209.1218459616989946 ) ) ;
#75918=CARTESIAN_POINT ( 'NONE',  ( 8.505021145809154248, 1364.171015757792247, 210.6218459617142003 ) ) ;
#75932=CARTESIAN_POINT ( 'NONE',  ( 7.445922712503920238, 1367.935115748522094, 210.6218459616991936 ) ) ;
#76064=CARTESIAN_POINT ( 'NONE',  ( -2.632747685671116944, 1389.413060387289988, 207.6835693458863830 ) ) ;
#76072=CARTESIAN_POINT ( 'NONE',  ( -7.173827098650000345, 1361.757975858899954, 207.6218459616989946 ) ) ;
#76110=VERTEX_POINT ( 'NONE', #11207 ) ;
#76190=CARTESIAN_POINT ( 'NONE',  ( -7.834163150019012534, 1364.423415641956353, 208.3718459617061285 ) ) ;
#76388=CARTESIAN_POINT ( 'NONE',  ( -9.184850993605149917E-16, 1374.913060387289988, 209.1218459616989946 ) ) ;
#76403=CARTESIAN_POINT ( 'NONE',  ( -4.234272664024971711, 1370.421201462527506, 209.6675854122346152 ) ) ;
#76468=CARTESIAN_POINT ( 'NONE',  ( 7.340269731178259427, 1361.836778001474158, 210.6218459616987957 ) ) ;
#76482=CARTESIAN_POINT ( 'NONE',  ( 8.988338641399998608, 1366.896325247149889, 207.6218459616989946 ) ) ;
#76606=DIRECTION ( 'NONE',  ( -1.407418274235000032E-17, -1.000000000000000000, 2.576261870300899651E-17 ) ) ;
#76616=CARTESIAN_POINT ( 'NONE',  ( 4.670493445319249481, 1358.850376296546983, 209.6218459617033432 ) ) ;
#76739=CARTESIAN_POINT ( 'NONE',  ( -8.537163784377359121, 1364.215151872246452, 210.6218459617142003 ) ) ;
#76747=CARTESIAN_POINT ( 'NONE',  ( -9.860907387307680239, 1368.605983359357424, 208.3718459617010978 ) ) ;
#77034=CARTESIAN_POINT ( 'NONE',  ( 8.602227872912603601, 1365.853205000053777, 207.6218459616988241 ) ) ;
#77048=SURFACE_STYLE_FILL_AREA ( #69771 ) ;
#77050=CARTESIAN_POINT ( 'NONE',  ( 6.995010115480782886, 1370.198628283411608, 208.3718459617010978 ) ) ;
#77151=VERTEX_POINT ( 'NONE', #74459 ) ;
#77185=CARTESIAN_POINT ( 'NONE',  ( -4.745098151931287589, 1360.923919868593885, 210.6218459616991936 ) ) ;
#77210=FACE_OUTER_BOUND ( 'NONE', #91597, .T. ) ;
#77304=CARTESIAN_POINT ( 'NONE',  ( -9.505471540889999460, 1363.500209798499782, 207.6218459616989946 ) ) ;
#77312=CARTESIAN_POINT ( 'NONE',  ( -8.232155009519999567, 1367.485244382299925, 207.6218459616989946 ) ) ;
#77366=DIRECTION ( 'NONE',  ( -0.8775825618903725367, 0.000000000000000000, -0.4794255386042032829 ) ) ;
#77535=( BOUNDED_CURVE ( )  B_SPLINE_CURVE ( 5, ( #98623, #55006, #29230, #73448, #37628, #98074 ),
 .UNSPECIFIED., .F., .T. ) 
 B_SPLINE_CURVE_WITH_KNOTS ( ( 6, 6 ),
 ( 0.000000000000000000, 1.000000000000000000 ),
 .UNSPECIFIED. ) 
 CURVE ( )  GEOMETRIC_REPRESENTATION_ITEM ( )  RATIONAL_B_SPLINE_CURVE ( ( 0.2685209231508545735, 0.2609802027898279753, 0.2554570136197181762, 0.2518190045398730481, 0.2499999999999668043, 0.2500000000000000000 ) ) 
 REPRESENTATION_ITEM ( '' )  );
#77537=FACE_OUTER_BOUND ( 'NONE', #47427, .T. ) ;
#77580=CARTESIAN_POINT ( 'NONE',  ( 8.126636070261570310, 1364.911473247693039, 208.3718459617061285 ) ) ;
#77595=CARTESIAN_POINT ( 'NONE',  ( 8.726849315049999944, 1367.111769039820047, 207.6218459616989946 ) ) ;
#77605=CARTESIAN_POINT ( 'NONE',  ( 9.258247136799999666, 1363.198586359130104, 207.6218459616989946 ) ) ;
#77726=CARTESIAN_POINT ( 'NONE',  ( -6.569693564645711525, 1359.476008147596986, 208.3718459617010978 ) ) ;
#77753=CARTESIAN_POINT ( 'NONE',  ( -4.297805644383835499, 1367.976344583816626, 207.6218459616988241 ) ) ;
#77847=CARTESIAN_POINT ( 'NONE',  ( -7.173827098684180115, 1361.757975858857890, 210.6218459616987957 ) ) ;
#77855=CARTESIAN_POINT ( 'NONE',  ( -10.21846136005779115, 1368.315982671009579, 208.3718459617010978 ) ) ;
#77883=ORIENTED_EDGE ( 'NONE', *, *, #3684, .F. ) ;
#78044=CARTESIAN_POINT ( 'NONE',  ( -3.034926079678273325, 1369.200812461397618, 207.6218459616989946 ) ) ;
#78057=VERTEX_POINT ( 'NONE', #108753 ) ;
#78067=DIRECTION ( 'NONE',  ( -0.4794255386042041156, 5.511896626706600487E-17, 0.8775825618903722036 ) ) ;
#78118=CARTESIAN_POINT ( 'NONE',  ( 8.985456466844782497, 1364.704792932128157, 207.6218459616988241 ) ) ;
#78130=( NAMED_UNIT ( * ) PLANE_ANGLE_UNIT ( ) SI_UNIT ( $, .RADIAN. ) );
#78132=CARTESIAN_POINT ( 'NONE',  ( 8.251048879689999893, 1367.474174444410210, 207.6218459616989946 ) ) ;
#78144=CARTESIAN_POINT ( 'NONE',  ( -8.232155009519999567, 1367.485244382299925, 207.6218459616989946 ) ) ;
#78237=ORIENTED_EDGE ( 'NONE', *, *, #82806, .F. ) ;
#78268=CARTESIAN_POINT ( 'NONE',  ( 0.05823133897989880153, 1360.390585217559874, 207.6218459616989946 ) ) ;
#78296=CARTESIAN_POINT ( 'NONE',  ( -7.811405798899279773, 1367.739269854455870, 210.6218459616987957 ) ) ;
#78382=CARTESIAN_POINT ( 'NONE',  ( -2.824362723775959427, 1367.715796969916255, 209.3184871409762309 ) ) ;
#78398=CARTESIAN_POINT ( 'NONE',  ( -7.592149787980000397, 1361.964468435470053, 207.6218459616989946 ) ) ;
#78406=CARTESIAN_POINT ( 'NONE',  ( -8.232155009518420385, 1367.485244382291967, 210.6218459616991936 ) ) ;
#78489=CARTESIAN_POINT ( 'NONE',  ( 4.362764246034863902, 1370.448454204201653, 209.4935560900470648 ) ) ;
#78502=CIRCLE ( 'NONE', #58835, 10.00000000000000888 ) ;
#78547=CARTESIAN_POINT ( 'NONE',  ( -10.02185219040000064, 1364.916310432309956, 210.6218459616991936 ) ) ;
#78591=ORIENTED_EDGE ( 'NONE', *, *, #17967, .F. ) ;
#78603=CARTESIAN_POINT ( 'NONE',  ( 0.000000000000000000, 1389.913060387289988, 209.1218459616989946 ) ) ;
#78618=ORIENTED_EDGE ( 'NONE', *, *, #14249, .T. ) ;
#78680=CARTESIAN_POINT ( 'NONE',  ( 8.808043405595423536, 1365.554312915578294, 207.6218459616988241 ) ) ;
#78709=CARTESIAN_POINT ( 'NONE',  ( -5.986709854369999917, 1361.264879806939916, 207.6218459616989946 ) ) ;
#78839=CARTESIAN_POINT ( 'NONE',  ( 0.06294878256441671649, 1358.513759169126160, 208.3718459617010978 ) ) ;
#78871=CARTESIAN_POINT ( 'NONE',  ( -4.078508008763815695, 1366.999314411288651, 209.6218459617148824 ) ) ;
#78875=CARTESIAN_POINT ( 'NONE',  ( 3.149414619133680482, 1370.221588481574372, 210.2153961732977905 ) ) ;
#78952=CARTESIAN_POINT ( 'NONE',  ( -3.007336967298251729, 1369.006237963355716, 210.6121239941897159 ) ) ;
#78969=CARTESIAN_POINT ( 'NONE',  ( -3.603740778195532624, 1362.725725758258250, 209.6218459617148824 ) ) ;
#78978=CARTESIAN_POINT ( 'NONE',  ( -8.784417309943542307, 1369.490261236509468, 209.6218459617033432 ) ) ;
#79019=FILL_AREA_STYLE_COLOUR ( '', #103519 ) ;
#79028=ORIENTED_EDGE ( 'NONE', *, *, #60483, .T. ) ;
#79097=CARTESIAN_POINT ( 'NONE',  ( 2.114990338821392868, 1370.171684715506444, 206.8534323859588824 ) ) ;
#79114=DIRECTION ( 'NONE',  ( 0.9900962604114871279, -0.1403901532130690244, 1.186453863995930381E-14 ) ) ;
#79115=CARTESIAN_POINT ( 'NONE',  ( -9.516636888329999877, 1366.309137899869938, 210.6218459616991936 ) ) ;
#79145=ORIENTED_EDGE ( 'NONE', *, *, #14249, .F. ) ;
#79245=CARTESIAN_POINT ( 'NONE',  ( 8.052903166426546022, 1365.111483269165774, 208.3718459617061285 ) ) ;
#79270=CARTESIAN_POINT ( 'NONE',  ( 9.971295257839999593, 1364.502667329740007, 207.6218459616989946 ) ) ;
#79351=CARTESIAN_POINT ( 'NONE',  ( -8.775825618903727587, 1374.031200045389824, 204.3275905756569841 ) ) ;
#79386=CARTESIAN_POINT ( 'NONE',  ( 9.093835586129998205, 1363.023136422000107, 207.6218459616989946 ) ) ;
#79394=CARTESIAN_POINT ( 'NONE',  ( 3.087661701989000029, 1369.842518917919961, 211.2713650144889925 ) ) ;
#79413=CARTESIAN_POINT ( 'NONE',  ( -7.690112133868802324, 1366.641875226467164, 207.6218459616988241 ) ) ;
#79476=( BOUNDED_CURVE ( )  B_SPLINE_CURVE ( 5, ( #9672, #87508, #10229, #11354, #97011, #69621, #35997, #105404, #28696, #1863, #62901, #54477, #53362, #79115, #88614, #44406, #3518, #37643, #96452, #78547, #104849, #105965, #61769, #19156, #2423, #36540, #70736, #62327, #98087, #81831, #82940, #72369, #12972, #64521, #91351, #14631, #39845, #72906, #106499, #4062, #99728, #38187, #13514, #108697, #21358, #48818, #40385, #63974, #107595, #31988, #55565, #12432, #29786, #98636, #21904, #38731, #89690, #22455, #6232, #66177, #46622, #74562, #47155, #81281, #80753, #65060, #47702, #89146, #5134, #4597, #5700, #39290, #107046, #23020, #30332, #20823, #56101, #90230 ),
 .UNSPECIFIED., .F., .F. ) 
 B_SPLINE_CURVE_WITH_KNOTS ( ( 6, 3, 3, 3, 3, 3, 3, 3, 3, 3, 3, 3, 3, 3, 3, 3, 3, 3, 3, 3, 3, 3, 3, 3, 3, 6 ),
 ( 0.03051383316186220829, 3.902585213099999617, 6.240861926940000082, 6.790072646650000543, 8.377982366400001268, 8.928580102349998882, 10.97133995140000096, 12.98949692179999893, 13.60228008900000063, 15.24737252870000148, 15.86745694640000259, 18.51059426890000026, 22.57641725190000059, 26.75087197449999721, 31.16005629229999840, 33.90953505430000092, 34.60237748540000524, 36.31249047570000243, 36.97255805550000218, 38.99052022429999909, 41.04947707190000017, 41.62972334150000364, 43.19545136810000230, 43.76106149099999953, 46.17824368760000908, 50.04091111600000374 ),
 .UNSPECIFIED. ) 
 CURVE ( )  GEOMETRIC_REPRESENTATION_ITEM ( )  RATIONAL_B_SPLINE_CURVE ( ( 0.2500000000000000000, 0.2500000000000000000, 0.2500000000000000000, 0.2500000000000000000, 0.2500000000000000000, 0.2500000000000000000, 0.2500000000000000000, 0.2500000000000000000, 0.2500000000000000000, 0.2500000000000000000, 0.2500000000000000000, 0.2500000000000000000, 0.2500000000000000000, 0.2500000000000000000, 0.2500000000000000000, 0.2500000000000000000, 0.2500000000000000000, 0.2500000000000000000, 0.2500000000000000000, 0.2500000000000000000, 0.2500000000000000000, 0.2500000000000000000, 0.2500000000000000000, 0.2500000000000000000, 0.2500000000000000000, 0.2500000000000000000, 0.2500000000000000000, 0.2500000000000000000, 0.2500000000000000000, 0.2500000000000000000, 0.2500000000000000000, 0.2500000000000000000, 0.2500000000000000000, 0.2500000000000000000, 0.2500000000000000000, 0.2500000000000000000, 0.2500000000000000000, 0.2500000000000000000, 0.2500000000000000000, 0.2500000000000000000, 0.2500000000000000000, 0.2500000000000000000, 0.2500000000000000000, 0.2500000000000000000, 0.2500000000000000000, 0.2500000000000000000, 0.2500000000000000000, 0.2500000000000000000, 0.2500000000000000000, 0.2500000000000000000, 0.2500000000000000000, 0.2500000000000000000, 0.2500000000000000000, 0.2500000000000000000, 0.2500000000000000000, 0.2500000000000000000, 0.2500000000000000000, 0.2500000000000000000, 0.2500000000000000000, 0.2500000000000000000, 0.2500000000000000000, 0.2500000000000000000, 0.2500000000000000000, 0.2500000000000000000, 0.2500000000000000000, 0.2500000000000000000, 0.2500000000000000000, 0.2500000000000000000, 0.2500000000000000000, 0.2500000000000000000, 0.2500000000000000000, 0.2500000000000000000, 0.2500000000000000000, 0.2500000000000000000, 0.2500000000000000000, 0.2500000000000000000, 0.2500000000000000000, 0.2500000000000000000 ) ) 
 REPRESENTATION_ITEM ( '' )  );
#79518=CARTESIAN_POINT ( 'NONE',  ( -11.16589708279419391, 1364.318862766833718, 210.6218459617030021 ) ) ;
#79760=DIRECTION ( 'NONE',  ( -1.407418274235009893E-17, -1.000000000000000000, 2.576261870300909820E-17 ) ) ;
#79798=CARTESIAN_POINT ( 'NONE',  ( 6.612365369791289638, 1366.252322145174958, 208.3718459617061285 ) ) ;
#79824=CARTESIAN_POINT ( 'NONE',  ( -5.247433916371702978, 1368.770886448055762, 207.6218459616990515 ) ) ;
#79937=CARTESIAN_POINT ( 'NONE',  ( 8.947167975125823958, 1361.631581952299712, 207.6218459616987673 ) ) ;
#79958=CARTESIAN_POINT ( 'NONE',  ( -7.622296587833937487, 1365.431469736285635, 209.6218459617148824 ) ) ;
#79993=DIRECTION ( 'NONE',  ( 0.4794255386042041156, -2.935634756405673411E-17, -0.8775825618903722036 ) ) ;
#80053=CARTESIAN_POINT ( 'NONE',  ( -11.13778651236117057, 1367.489867554787679, 209.6218459617033432 ) ) ;
#80105=ADVANCED_FACE ( 'NONE', ( #10320 ), #69354, .T. ) ;
#80134=CARTESIAN_POINT ( 'NONE',  ( 4.408076783308741753, 1370.458220770605067, 208.8302519701303765 ) ) ;
#80340=CARTESIAN_POINT ( 'NONE',  ( 4.501691961449999724, 1368.956319095359959, 207.6218459616989946 ) ) ;
#80367=CARTESIAN_POINT ( 'NONE',  ( 9.704582620010000937, 1366.001145740639913, 207.6218459616989946 ) ) ;
#80491=CARTESIAN_POINT ( 'NONE',  ( 9.995873456701064086, 1362.519969852305167, 207.6218459616987673 ) ) ;
#80514=CARTESIAN_POINT ( 'NONE',  ( -8.048119939141594514, 1365.119509101891254, 208.3718459617061285 ) ) ;
#80566=DIRECTION ( 'NONE',  ( 0.1403878024439506045, 0.9900965937346509760, 0.000000000000000000 ) ) ;
#80610=CARTESIAN_POINT ( 'NONE',  ( -9.657355732020000971, 1366.083296228050131, 207.6218459616989946 ) ) ;
#80647=EDGE_LOOP ( 'NONE', ( #38741, #70286, #13443, #87324, #72416, #21987, #97282, #79028 ) ) ;
#80715=FACE_OUTER_BOUND ( 'NONE', #59665, .T. ) ;
#80753=CARTESIAN_POINT ( 'NONE',  ( 9.532517564019999057, 1366.286862064870093, 210.6218459616991936 ) ) ;
#80888=CARTESIAN_POINT ( 'NONE',  ( 7.637356462754751441, 1365.417503186476779, 209.6218459617148824 ) ) ;
#80929=EDGE_LOOP ( 'NONE', ( #105103, #95463, #108422, #33606 ) ) ;
#81015=CARTESIAN_POINT ( 'NONE',  ( -3.627397453644670033, 1362.602819439402992, 208.3718459617061285 ) ) ;
#81029=CARTESIAN_POINT ( 'NONE',  ( 9.093835586142619221, 1363.023136422003972, 210.6218459616991936 ) ) ;
#81048=CARTESIAN_POINT ( 'NONE',  ( -8.000983929430127262, 1364.900167260016815, 209.6218459617148824 ) ) ;
#81146=CARTESIAN_POINT ( 'NONE',  ( -9.830395177430000686, 1365.769828494180047, 207.6218459616989946 ) ) ;
#81168=ORIENTED_EDGE ( 'NONE', *, *, #8381, .F. ) ;
#81281=CARTESIAN_POINT ( 'NONE',  ( 9.671060821790000261, 1366.060403940050037, 210.6218459616991936 ) ) ;
#81348=DIRECTION ( 'NONE',  ( 3.828568698926945491E-16, 0.000000000000000000, -1.000000000000000000 ) ) ;
#81406=CARTESIAN_POINT ( 'NONE',  ( 7.721792848913118235, 1365.509929565264883, 208.3718459617061285 ) ) ;
#81432=CARTESIAN_POINT ( 'NONE',  ( 9.231361398829999843, 1366.659448741839924, 207.6218459616989946 ) ) ;
#81546=CARTESIAN_POINT ( 'NONE',  ( -3.982247585420000124, 1360.759224656429978, 207.6218459616989946 ) ) ;
#81563=CARTESIAN_POINT ( 'NONE',  ( 9.943976501839999926, 1365.461622992600041, 207.6218459616989946 ) ) ;
#81586=CARTESIAN_POINT ( 'NONE',  ( -9.830395177430000686, 1365.769828494180047, 207.6218459616989946 ) ) ;
#81609=CARTESIAN_POINT ( 'NONE',  ( -2.813822098188480059, 1367.641464703512383, 209.1220808600859300 ) ) ;
#81684=CARTESIAN_POINT ( 'NONE',  ( -10.51561482155124772, 1366.597316028666000, 207.6218459616987673 ) ) ;
#81831=CARTESIAN_POINT ( 'NONE',  ( -8.622403150220000256, 1362.632156860360055, 210.6218459616991936 ) ) ;
#81862=ORIENTED_EDGE ( 'NONE', *, *, #108310, .T. ) ;
#81966=CARTESIAN_POINT ( 'NONE',  ( 8.251048879689999893, 1367.474174444410210, 207.6218459616989946 ) ) ;
#82107=CARTESIAN_POINT ( 'NONE',  ( -2.380813228430795903, 1360.502616939869995, 210.6218459616987957 ) ) ;
#82122=CARTESIAN_POINT ( 'NONE',  ( 10.02176186330000007, 1364.879735892739973, 207.6218459616989946 ) ) ;
#82147=CARTESIAN_POINT ( 'NONE',  ( -9.832966357676340863, 1364.062280235945991, 210.6218459616987957 ) ) ;
#82255=CARTESIAN_POINT ( 'NONE',  ( -7.592149787962600094, 1361.964468435472099, 210.6218459616991936 ) ) ;
#82386=CARTESIAN_POINT ( 'NONE',  ( 8.337034337958543873, 1374.413060387289988, 213.6763885784389174 ) ) ;
#82670=CARTESIAN_POINT ( 'NONE',  ( 0.05571536906665219835, 1361.391559110059688, 207.6218459616988241 ) ) ;
#82686=CARTESIAN_POINT ( 'NONE',  ( 10.72817992001798970, 1363.601820912770791, 207.6218459616987673 ) ) ;
#82708=CARTESIAN_POINT ( 'NONE',  ( -8.627444824590488892, 1365.466472467317772, 210.6218459617142003 ) ) ;
#82802=CARTESIAN_POINT ( 'NONE',  ( -10.52246697409539422, 1361.794959946351355, 208.3718459617010978 ) ) ;
#82806=EDGE_CURVE ( 'NONE', #74455, #7609, #96263, .T. ) ;
#82817=DIRECTION ( 'NONE',  ( -6.123233995736769734E-17, -1.000000000000000000, -1.124819836996399911E-32 ) ) ;
#82940=CARTESIAN_POINT ( 'NONE',  ( -8.538839991170000587, 1362.569232148550100, 210.6218459616991936 ) ) ;
#82980=VECTOR ( 'NONE', #30091, 1000.000000000000000 ) ;
#82988=ORIENTED_EDGE ( 'NONE', *, *, #4208, .F. ) ;
#83042=CARTESIAN_POINT ( 'NONE',  ( -9.724834716106559089E-16, 1374.031200045389824, 209.1218459616989946 ) ) ;
#83152=B_SPLINE_CURVE_WITH_KNOTS ( 'NONE', 3,
 ( #105804, #86776, #78952, #29084, #69454, #10065, #95731, #17891, #52089, #36921, #70014, #26873, #78382, #45356, #9511, #1139, #35270, #61064, #1690, #53193, #35831, #87903, #2258, #104680, #36373, #70562 ),
 .UNSPECIFIED., .F., .F.,
 ( 4, 2, 2, 2, 2, 2, 2, 2, 2, 2, 2, 2, 4 ),
 ( 1.683460768918727255E-14, 0.0002930453684808659613, 0.0005860907369448972986, 0.0008791361054089286359, 0.001172181473872959973, 0.001758272210801022648, 0.002344362947729085322, 0.002637408316193116768, 0.002930453684657148214, 0.003223499053121179660, 0.003516544421585210672, 0.004102635158513215884, 0.004688725895441220662 ),
 .UNSPECIFIED. ) ;
#83217=CARTESIAN_POINT ( 'NONE',  ( 7.942782220523640468, 1364.774038235526405, 209.6218459617148824 ) ) ;
#83233=CARTESIAN_POINT ( 'NONE',  ( 11.28921847714573801, 1367.009324610933390, 208.3718459617010978 ) ) ;
#83351=CARTESIAN_POINT ( 'NONE',  ( -11.32426234103323992, 1362.877771080770117, 208.3718459617010978 ) ) ;
#83379=ORIENTED_EDGE ( 'NONE', *, *, #102828, .T. ) ;
#83480=CARTESIAN_POINT ( 'NONE',  ( -4.098601998020408921, 1370.943769148376759, 208.3718459617010978 ) ) ;
#83626=EDGE_CURVE ( 'NONE', #9968, #78057, #57525, .T. ) ;
#83696=CARTESIAN_POINT ( 'NONE',  ( -3.180365954810094209, 1370.226539215819685, 208.0370721656823321 ) ) ;
#83713=SHAPE_REPRESENTATION ( 'Handle Screw', ( #21632 ), #103904 ) ;
#83765=CARTESIAN_POINT ( 'NONE',  ( 7.776966983056124327, 1363.498993241026710, 210.6218459617142003 ) ) ;
#83770=ORIENTED_EDGE ( 'NONE', *, *, #46877, .F. ) ;
#83782=CARTESIAN_POINT ( 'NONE',  ( 9.842969107811420315, 1365.740588703662070, 210.6218459616991936 ) ) ;
#83800=CARTESIAN_POINT ( 'NONE',  ( -0.8539859765994225471, 1391.413060387289988, 209.6421419849122572 ) ) ;
#83860=( GEOMETRIC_REPRESENTATION_CONTEXT ( 3 ) GLOBAL_UNCERTAINTY_ASSIGNED_CONTEXT ( ( #68184 ) ) GLOBAL_UNIT_ASSIGNED_CONTEXT ( ( #2320, #20714, #12879 ) ) REPRESENTATION_CONTEXT ( 'NONE', 'WORKASPACE' ) );
#83905=CARTESIAN_POINT ( 'NONE',  ( -9.328535443860001664, 1363.278783432130012, 207.6218459616989946 ) ) ;
#84167=DIRECTION ( 'NONE',  ( 0.1215789942062129869, 0.8574459172214418112, -0.5000050471826120724 ) ) ;
#84289=TOROIDAL_SURFACE ( 'NONE', #95008, 3.500000000000000000, 0.5000000000000000000 ) ;
#84314=CARTESIAN_POINT ( 'NONE',  ( 8.373095552927001251, 1364.012926167303931, 210.6218459617142003 ) ) ;
#84329=CARTESIAN_POINT ( 'NONE',  ( 9.266584390650891123, 1367.960107183285118, 207.6218459616987673 ) ) ;
#84353=MANIFOLD_SOLID_BREP ( 'Stock-MAS-682-1', #86002 ) ;
#84373=ORIENTED_EDGE ( 'NONE', *, *, #45523, .T. ) ;
#84428=ORIENTED_EDGE ( 'NONE', *, *, #63757, .T. ) ;
#84464=CARTESIAN_POINT ( 'NONE',  ( -8.622403150218080015, 1362.632156860364148, 210.6218459616991936 ) ) ;
#84579=CARTESIAN_POINT ( 'NONE',  ( -7.893155011514420671, 1363.585497717410817, 210.6218459617142003 ) ) ;
#84610=PLANE ( 'NONE',  #65091 ) ;
#84793=AXIS2_PLACEMENT_3D ( 'NONE', #6672, #41391, #40272 ) ;
#84846=CARTESIAN_POINT ( 'NONE',  ( 8.803103321107110801, 1364.263256477290497, 207.6218459616988241 ) ) ;
#84863=CARTESIAN_POINT ( 'NONE',  ( 5.738076989630942037, 1370.712929383438905, 209.6218459617033432 ) ) ;
#84943=EDGE_LOOP ( 'NONE', ( #64838, #32150, #93702, #91078 ) ) ;
#85000=CARTESIAN_POINT ( 'NONE',  ( -3.982247585420000124, 1360.759224656429978, 207.6218459616989946 ) ) ;
#85118=ORIENTED_EDGE ( 'NONE', *, *, #28769, .T. ) ;
#85126=CARTESIAN_POINT ( 'NONE',  ( -7.592149787973779596, 1361.964468435450044, 210.6218459616987957 ) ) ;
#85136=CARTESIAN_POINT ( 'NONE',  ( -7.811405798920000088, 1367.739269854440181, 207.6218459616989946 ) ) ;
#85169=CARTESIAN_POINT ( 'NONE',  ( -0.5481912525510364009, 1370.039449668079669, 211.2584053860457232 ) ) ;
#85225=VECTOR ( 'NONE', #6811, 1000.000000000000000 ) ;
#85399=CARTESIAN_POINT ( 'NONE',  ( 9.454737631267599696, 1363.431170718773956, 210.6218459616987957 ) ) ;
#85414=CARTESIAN_POINT ( 'NONE',  ( 3.756023522790000069, 1369.098589419769951, 207.6218459616989946 ) ) ;
#85480=CARTESIAN_POINT ( 'NONE',  ( 8.578717400394859958E-16, 1374.913060387289988, 209.1218459616989946 ) ) ;
#85548=CARTESIAN_POINT ( 'NONE',  ( -6.608559145320131556, 1359.356750036984067, 209.6218459617033432 ) ) ;
#85573=ORIENTED_EDGE ( 'NONE', *, *, #39109, .F. ) ;
#85657=CYLINDRICAL_SURFACE ( 'NONE', #49937, 2.999999999999999556 ) ;
#85675=AXIS2_PLACEMENT_3D ( 'NONE', #38949, #23255, #57454 ) ;
#85679=CARTESIAN_POINT ( 'NONE',  ( -7.482952933474933843, 1364.121751949525560, 208.3718459617061285 ) ) ;
#85687=CARTESIAN_POINT ( 'NONE',  ( -10.56833826840790813, 1367.981913465304388, 208.3718459617010978 ) ) ;
#85971=CARTESIAN_POINT ( 'NONE',  ( 7.985371214169377119, 1364.849800335405234, 209.6218459617148824 ) ) ;
#85986=CARTESIAN_POINT ( 'NONE',  ( 10.25488443387654591, 1368.282720929027164, 208.3718459617010978 ) ) ;
#85996=CARTESIAN_POINT ( 'NONE',  ( -7.592149787980000397, 1361.964468435470053, 207.6218459616989946 ) ) ;
#86002=CLOSED_SHELL ( 'NONE', ( #48619, #80105, #17848, #73671, #19683, #13688, #11151, #35039, #8423, #65922, #100749, #48302, #6414, #807, #33664, #59168, #12083, #92443, #73292, #86052, #57726, #71274, #15693, #64961 ) ) ;
#86031=CIRCLE ( 'NONE', #55617, 3.000000000000002665 ) ;
#86052=ADVANCED_FACE ( 'NONE', ( #24239 ), #105467, .F. ) ;
#86121=CARTESIAN_POINT ( 'NONE',  ( -4.209351669747369407, 1359.579323995338200, 210.6218459617030021 ) ) ;
#86145=CARTESIAN_POINT ( 'NONE',  ( -7.850666375130202823, 1365.384408210369429, 208.3718459617061285 ) ) ;
#86235=CARTESIAN_POINT ( 'NONE',  ( -7.562440734658915531, 1363.099625272887806, 207.6218459616988241 ) ) ;
#86243=CARTESIAN_POINT ( 'NONE',  ( -9.232879690934204575, 1367.985994792911470, 207.6218459616987673 ) ) ;
#86270=ORIENTED_EDGE ( 'NONE', *, *, #18154, .F. ) ;
#86288=EDGE_CURVE ( 'NONE', #437, #39065, #87636, .T. ) ;
#86513=B_SPLINE_CURVE_WITH_KNOTS ( 'NONE', 5,
 ( #70341, #69216, #1446, #79824, #51860, #60830, #10956, #78144, #71457, #87101, #103326, #43458, #36157, #36702, #19884, #45128, #10388, #27201, #69783, #61937, #54091, #11510, #913, #88216, #61383, #97158, #105573, #63054, #52419, #35591, #53525, #9840, #85996, #104453, #78709, #44559, #96616, #3130, #26633, #95502, #70896, #9295, #45685, #105012, #103901, #52969, #94954, #2022, #44007, #87667, #37260, #77605, #86546, #27745, #96054, #18224, #19324, #79270, #2580, #28301, #62495, #28860, #80367, #89309, #22065, #97707, #81432, #4743, #39458, #74182, #46234, #21522, #107761, #99338, #106649, #5863, #56262, #29389 ),
 .UNSPECIFIED., .F., .F.,
 ( 6, 3, 3, 3, 3, 3, 3, 3, 3, 3, 3, 3, 3, 3, 3, 3, 3, 3, 3, 3, 3, 3, 3, 3, 3, 6 ),
 ( 0.03051383316132079068, 3.902585213099999617, 6.240861926939999194, 6.790072646649998767, 8.377982366400001268, 8.928580102349998882, 10.97133995140000096, 12.98949692180000071, 13.60228008900000063, 15.24737252870000148, 15.86745694640000082, 18.51059426890000026, 22.57641725190000415, 26.75087197450000076, 31.16005629229999840, 33.90953505430000092, 34.60237748540000524, 36.31249047570000243, 36.97255805550000218, 38.99052022429999909, 41.04947707190000017, 41.62972334149999654, 43.19545136810000230, 43.76106149099999953, 46.17824368760000198, 50.04091111600000374 ),
 .UNSPECIFIED. ) ;
#86520=CARTESIAN_POINT ( 'NONE',  ( 8.916609868645085868, 1365.352032791107831, 207.6218459616988241 ) ) ;
#86534=CARTESIAN_POINT ( 'NONE',  ( 8.726849315034220567, 1367.111769039812089, 210.6218459616991936 ) ) ;
#86546=CARTESIAN_POINT ( 'NONE',  ( 9.454737631249999552, 1363.431170718789872, 207.6218459616989946 ) ) ;
#86603=DIRECTION ( 'NONE',  ( 3.828568698926945984E-16, 0.000000000000000000, -1.000000000000000000 ) ) ;
#86667=CARTESIAN_POINT ( 'NONE',  ( -7.673282386996102211, 1360.664745917332993, 210.6218459617030021 ) ) ;
#86695=CARTESIAN_POINT ( 'NONE',  ( -4.921072290514207026, 1367.614687051687270, 210.6218459617142003 ) ) ;
#86776=CARTESIAN_POINT ( 'NONE',  ( -3.021015307306127884, 1369.102705570917351, 210.6218459617000462 ) ) ;
#86791=CARTESIAN_POINT ( 'NONE',  ( -9.655745333040000489, 1363.739547551590022, 207.6218459616989946 ) ) ;
#86799=CARTESIAN_POINT ( 'NONE',  ( -9.354513558941972562, 1368.144804009614290, 210.6218459617030021 ) ) ;
#86856=DIRECTION ( 'NONE',  ( 0.4794255386042040046, -5.511896626706599255E-17, -0.8775825618903723147 ) ) ;
#87078=CARTESIAN_POINT ( 'NONE',  ( 8.770701337765752115, 1364.659332542723632, 210.6218459617142003 ) ) ;
#87101=CARTESIAN_POINT ( 'NONE',  ( -8.696701630030000629, 1367.135748871429996, 207.6218459616989946 ) ) ;
#87229=CARTESIAN_POINT ( 'NONE',  ( -3.982247585415259916, 1360.759224656435890, 210.6218459616991936 ) ) ;
#87254=CARTESIAN_POINT ( 'NONE',  ( -6.371134682390000137, 1368.423166410909971, 207.6218459616989946 ) ) ;
#87284=CIRCLE ( 'NONE', #53329, 18.16666666670000296 ) ;
#87324=ORIENTED_EDGE ( 'NONE', *, *, #72662, .F. ) ;
#87352=CARTESIAN_POINT ( 'NONE',  ( -0.7212203791732667568, 1361.603923786195764, 210.6218459617142003 ) ) ;
#87360=CARTESIAN_POINT ( 'NONE',  ( -5.728941678023104167, 1370.586255878621841, 208.3718459617010978 ) ) ;
#87444=CARTESIAN_POINT ( 'NONE',  ( 3.297000113654319886, 1370.245087421812514, 208.0695929694545043 ) ) ;
#87462=TOROIDAL_SURFACE ( 'NONE', #19412, 21.40691501530000096, 1.500287545629999997 ) ;
#87508=CARTESIAN_POINT ( 'NONE',  ( -3.787329988060110342, 1369.092969256073502, 210.6218459616991936 ) ) ;
#87636=CIRCLE ( 'NONE', #110796, 0.4999999999999980016 ) ;
#87643=CARTESIAN_POINT ( 'NONE',  ( 8.123801262052971595, 1364.937873541178078, 208.3718459617061285 ) ) ;
#87667=CARTESIAN_POINT ( 'NONE',  ( 8.796059898609998484, 1362.759824263850078, 207.6218459616989946 ) ) ;
#87762=AXIS2_PLACEMENT_3D ( 'NONE', #69542, #26961, #61151 ) ;
#87799=CARTESIAN_POINT ( 'NONE',  ( 8.379275254590000443, 1362.454991452509830, 207.6218459616989946 ) ) ;
#87826=CARTESIAN_POINT ( 'NONE',  ( -7.894907142693425861, 1366.239093409125644, 210.6218459617142003 ) ) ;
#87881=CARTESIAN_POINT ( 'NONE',  ( 5.561733859871847763, 1387.291117539184825, 209.1218459616989946 ) ) ;
#87903=CARTESIAN_POINT ( 'NONE',  ( -2.905551374272877130, 1368.288386645854189, 207.9218722600712965 ) ) ;
#87919=CARTESIAN_POINT ( 'NONE',  ( -5.986709854334679726, 1361.264879806951967, 210.6218459616987957 ) ) ;
#87928=CARTESIAN_POINT ( 'NONE',  ( -10.55984826015959221, 1366.521027767394116, 207.6218459616987673 ) ) ;
#87936=ORIENTED_EDGE ( 'NONE', *, *, #69028, .F. ) ;
#87996=AXIS2_PLACEMENT_3D ( 'NONE', #75860, #108908, #101583 ) ;
#88191=CARTESIAN_POINT ( 'NONE',  ( 7.834673235704612715, 1365.208883084832678, 209.6218459617148824 ) ) ;
#88206=CARTESIAN_POINT ( 'NONE',  ( 3.934203666168589297, 1370.083327362674481, 207.6218459616987673 ) ) ;
#88216=CARTESIAN_POINT ( 'NONE',  ( -9.692061980449999226, 1363.802329763670059, 207.6218459616989946 ) ) ;
#88334=CARTESIAN_POINT ( 'NONE',  ( 9.258247136794901522, 1363.198586359130104, 210.6218459616991936 ) ) ;
#88359=CARTESIAN_POINT ( 'NONE',  ( -7.227598892266946962, 1366.688675025208795, 210.6218459617142003 ) ) ;
#88361=ORIENTED_EDGE ( 'NONE', *, *, #39109, .T. ) ;
#88462=CARTESIAN_POINT ( 'NONE',  ( -11.42967626019537519, 1367.015145146939176, 209.6218459617033432 ) ) ;
#88547=CARTESIAN_POINT ( 'NONE',  ( 3.861717407563222793, 1370.346415241654313, 208.3041812415887932 ) ) ;
#88581=EDGE_CURVE ( 'NONE', #15971, #36895, #36709, .T. ) ;
#88594=CARTESIAN_POINT ( 'NONE',  ( 0.5076376709490001415, 1370.038171240497604, 206.9860627148225376 ) ) ;
#88613=DIRECTION ( 'NONE',  ( 0.1403901532130616969, 0.9900962604114879051, 0.000000000000000000 ) ) ;
#88614=CARTESIAN_POINT ( 'NONE',  ( -9.657355732019999195, 1366.083296228050131, 210.6218459616991936 ) ) ;
#88623=ORIENTED_EDGE ( 'NONE', *, *, #27140, .T. ) ;
#88741=CARTESIAN_POINT ( 'NONE',  ( 9.231361398851440470, 1366.659448741856067, 210.6218459616987957 ) ) ;
#88883=CARTESIAN_POINT ( 'NONE',  ( 10.69580974240662563, 1363.139536609160814, 210.6218459617030021 ) ) ;
#88903=CARTESIAN_POINT ( 'NONE',  ( -8.646226660069116221, 1365.433969532401761, 210.6218459617142003 ) ) ;
#88920=VERTEX_POINT ( 'NONE', #50992 ) ;
#88996=CARTESIAN_POINT ( 'NONE',  ( -9.934709065784959492, 1365.494406819940195, 210.6218459616991936 ) ) ;
#89057=FACE_OUTER_BOUND ( 'NONE', #33112, .T. ) ;
#89146=CARTESIAN_POINT ( 'NONE',  ( 8.988338641399998608, 1366.896325247149889, 210.6218459616991936 ) ) ;
#89280=CARTESIAN_POINT ( 'NONE',  ( 8.988338641399998608, 1366.896325247149889, 207.6218459616989946 ) ) ;
#89295=CARTESIAN_POINT ( 'NONE',  ( 8.272555700608019129E-16, 1374.413060387289988, 209.1218459616989946 ) ) ;
#89309=CARTESIAN_POINT ( 'NONE',  ( 9.671060821790000261, 1366.060403940050037, 207.6218459616989946 ) ) ;
#89433=CARTESIAN_POINT ( 'NONE',  ( 10.14339872067701975, 1362.384246550940361, 210.6218459617030021 ) ) ;
#89455=CARTESIAN_POINT ( 'NONE',  ( -9.936738324562218949, 1364.340818343083811, 210.6218459616987957 ) ) ;
#89552=CARTESIAN_POINT ( 'NONE',  ( -11.87249271966457620, 1363.781469426163085, 209.6218459617033432 ) ) ;
#89690=CARTESIAN_POINT ( 'NONE',  ( 9.925983360900000108, 1364.303202023259928, 210.6218459616991936 ) ) ;
#89691=AXIS2_PLACEMENT_3D ( 'NONE', #38571, #72748, #106877 ) ;
#89702=LINE ( 'NONE', #65071, #20567 ) ;
#89732=CARTESIAN_POINT ( 'NONE',  ( -3.180365954794715400, 1370.226539215816501, 210.2066197577219100 ) ) ;
#89827=CARTESIAN_POINT ( 'NONE',  ( 5.215187551932488397, 1368.779556716660181, 210.6218459616987957 ) ) ;
#89844=DIRECTION ( 'NONE',  ( 3.828568698926946970E-16, 0.000000000000000000, -1.000000000000000000 ) ) ;
#89959=CARTESIAN_POINT ( 'NONE',  ( 5.604365146386656171, 1361.139420828382072, 210.6218459616987957 ) ) ;
#89964=EDGE_LOOP ( 'NONE', ( #109952, #60149, #69270, #60114, #95536, #48043, #77883, #14858 ) ) ;
#89975=CARTESIAN_POINT ( 'NONE',  ( 8.468955835539853538, 1361.070818662583406, 210.6218459617030021 ) ) ;
#89998=CARTESIAN_POINT ( 'NONE',  ( -8.820192260065399026, 1365.532793008303315, 207.6218459616988241 ) ) ;
#90090=CARTESIAN_POINT ( 'NONE',  ( -11.67265150915122085, 1366.570619958580210, 209.6218459617033432 ) ) ;
#90230=CARTESIAN_POINT ( 'NONE',  ( 3.005276066430000448, 1369.205039411269809, 210.6218459616989946 ) ) ;
#90365=CARTESIAN_POINT ( 'NONE',  ( 3.542207350731675586, 1367.916903888309889, 210.6218459617142003 ) ) ;
#90406=DIRECTION ( 'NONE',  ( 3.828568698926946970E-16, 0.000000000000000000, -1.000000000000000000 ) ) ;
#90505=CARTESIAN_POINT ( 'NONE',  ( 3.879721387549549760, 1362.649618568975711, 208.3718459617061285 ) ) ;
#90523=CARTESIAN_POINT ( 'NONE',  ( 11.15430180702570517, 1364.260116606875727, 210.6218459617030021 ) ) ;
#90536=ORIENTED_EDGE ( 'NONE', *, *, #36956, .F. ) ;
#90546=CARTESIAN_POINT ( 'NONE',  ( -8.989161040693090854, 1364.724223069021491, 207.6218459616988241 ) ) ;
#90629=CYLINDRICAL_SURFACE ( 'NONE', #89691, 9.999999999999992895 ) ;
#90646=CARTESIAN_POINT ( 'NONE',  ( -10.84079470823281000, 1361.963018199176304, 209.6218459617033432 ) ) ;
#90754=ORIENTED_EDGE ( 'NONE', *, *, #17967, .T. ) ;
#90816=CARTESIAN_POINT ( 'NONE',  ( -2.134964941497456969, 1389.913060387289988, 210.4225860197314830 ) ) ;
#90827=CARTESIAN_POINT ( 'NONE',  ( -3.034926079678203159, 1369.200812461396481, 210.6218459616991936 ) ) ;
#90837=ORIENTED_EDGE ( 'NONE', *, *, #104085, .F. ) ;
#91055=CARTESIAN_POINT ( 'NONE',  ( -0.6983432080223432870, 1362.279204239127239, 208.3718459617061285 ) ) ;
#91074=CARTESIAN_POINT ( 'NONE',  ( 10.95460019480790592, 1366.206855798723154, 210.6218459617030021 ) ) ;
#91078=ORIENTED_EDGE ( 'NONE', *, *, #372, .F. ) ;
#91102=CARTESIAN_POINT ( 'NONE',  ( -9.936738324559998503, 1364.340818343090177, 207.6218459616989946 ) ) ;
#91205=CARTESIAN_POINT ( 'NONE',  ( -10.14614043715151581, 1361.444406935758934, 208.3718459617010978 ) ) ;
#91274=CARTESIAN_POINT ( 'NONE',  ( -0.01912654351157340102, 1347.931987472819856, 209.1220808601199792 ) ) ;
#91351=CARTESIAN_POINT ( 'NONE',  ( -5.986709854329999914, 1361.264879806969930, 210.6218459616991936 ) ) ;
#91489=CARTESIAN_POINT ( 'NONE',  ( 2.836810703500213027, 1368.016923498806364, 210.6218459617142003 ) ) ;
#91597=EDGE_LOOP ( 'NONE', ( #95592, #32594, #85118, #59758 ) ) ;
#91614=CARTESIAN_POINT ( 'NONE',  ( 7.970805622722147099, 1364.587178592252030, 208.3718459617061285 ) ) ;
#91631=CARTESIAN_POINT ( 'NONE',  ( 9.984115569220000097, 1365.258395869459946, 207.6218459616989946 ) ) ;
#91752=CARTESIAN_POINT ( 'NONE',  ( -9.895196081809372046, 1362.408266275323513, 207.6218459616987673 ) ) ;
#91818=B_SPLINE_CURVE_WITH_KNOTS ( 'NONE', 3,
 ( #6449, #40595, #22656, #101035, #32197, #66380, #76403, #99381, #57429, #24334, #50121, #16466, #48469, #42256, #8088, #92102, #15378, #58515, #65818, #49567, #101582, #83696 ),
 .UNSPECIFIED., .F., .F.,
 ( 4, 2, 2, 2, 2, 2, 2, 2, 2, 2, 4 ),
 ( 3.231953689032543100E-05, 0.0004825677620379821304, 0.0009328159871856388230, 0.001383064212333296600, 0.001608188324907083204, 0.001833312437480870243, 0.002058436550054657064, 0.002283560662628443452, 0.002733808887776098193, 0.003184057112923752934, 0.003634305338071407675 ),
 .UNSPECIFIED. ) ;
#91919=CIRCLE ( 'NONE', #84793, 17.27637083661241135 ) ;
#92027=LINE ( 'NONE', #39418, #43267 ) ;
#92102=CARTESIAN_POINT ( 'NONE',  ( -4.240793048770994389, 1370.422564428242140, 208.5825087046766555 ) ) ;
#92167=CARTESIAN_POINT ( 'NONE',  ( 7.782994496996333389, 1364.555819372772248, 209.6218459617148824 ) ) ;
#92183=CARTESIAN_POINT ( 'NONE',  ( 9.671060821791741091, 1366.060403940048218, 210.6218459616991936 ) ) ;
#92265=AXIS2_PLACEMENT_3D ( 'NONE', #73536, #47222, #81348 ) ;
#92302=CARTESIAN_POINT ( 'NONE',  ( -8.602688007017421867, 1361.384357301913269, 207.6218459616987673 ) ) ;
#92354=CARTESIAN_POINT ( 'NONE',  ( -2.632747685671117832, 1375.413060387289988, 207.6835693458863830 ) ) ;
#92429=AXIS2_PLACEMENT_3D ( 'NONE', #70098, #86856, #18524 ) ;
#92443=ADVANCED_FACE ( 'NONE', ( #48661 ), #90629, .T. ) ;
#92455=VERTEX_POINT ( 'NONE', #33466 ) ;
#92635=CIRCLE ( 'NONE', #97981, 2.500000000000002220 ) ;
#92683=CARTESIAN_POINT ( 'NONE',  ( -0.01912637926573700076, 1347.932035898419826, 206.1218459616989946 ) ) ;
#92690=ORIENTED_EDGE ( 'NONE', *, *, #104758, .T. ) ;
#92709=CARTESIAN_POINT ( 'NONE',  ( 8.032334214226272806, 1363.687929514241205, 210.6218459617142003 ) ) ;
#92725=CARTESIAN_POINT ( 'NONE',  ( 11.39709565417286363, 1367.072585988989204, 209.6218459617033432 ) ) ;
#92856=CARTESIAN_POINT ( 'NONE',  ( -9.178315062050000250, 1363.109187794150102, 207.6218459616989946 ) ) ;
#92875=EDGE_CURVE ( 'NONE', #98602, #36895, #92027, .T. ) ;
#92978=CARTESIAN_POINT ( 'NONE',  ( -9.178315062074918984, 1363.109187794137824, 210.6218459616987957 ) ) ;
#93105=DIRECTION ( 'NONE',  ( -5.168774739196950157E-16, 1.261506706387156225E-22, 1.000000000000000000 ) ) ;
#93229=EDGE_CURVE ( 'NONE', #92455, #3293, #64384, .T. ) ;
#93263=CARTESIAN_POINT ( 'NONE',  ( 8.035765206089191537, 1364.685966892704982, 208.3718459617061285 ) ) ;
#93276=CARTESIAN_POINT ( 'NONE',  ( 5.476632270752042508, 1369.746243050054318, 207.6218459616987673 ) ) ;
#93319=DIRECTION ( 'NONE',  ( -3.828568698926946970E-16, 0.000000000000000000, 1.000000000000000000 ) ) ;
#93407=CARTESIAN_POINT ( 'NONE',  ( 1.826803300828446330, 1359.441796170313637, 207.6218459616987673 ) ) ;
#93523=CARTESIAN_POINT ( 'NONE',  ( -7.826634146540749626, 1363.535366961594946, 210.6218459617142003 ) ) ;
#93611=EDGE_LOOP ( 'NONE', ( #17424, #81862, #58147, #84373, #39150, #1730, #39363, #62082, #61650, #90536 ) ) ;
#93702=ORIENTED_EDGE ( 'NONE', *, *, #104085, .T. ) ;
#93748=DIRECTION ( 'NONE',  ( 0.8775825618903732028, -4.965288137873349002E-32, 0.4794255386042021172 ) ) ;
#93795=CARTESIAN_POINT ( 'NONE',  ( 7.877099145841899741, 1362.118768394163908, 210.6218459616987957 ) ) ;
#93807=( LENGTH_UNIT ( ) NAMED_UNIT ( * ) SI_UNIT ( .MILLI., .METRE. ) );
#93809=CARTESIAN_POINT ( 'NONE',  ( 8.251048879697160388, 1367.474174444406117, 210.6218459616991936 ) ) ;
#93956=CARTESIAN_POINT ( 'NONE',  ( 5.944559947674049383, 1359.984290312718713, 210.6218459617030021 ) ) ;
#93985=VERTEX_POINT ( 'NONE', #94103 ) ;
#94019=CARTESIAN_POINT ( 'NONE',  ( 3.145310910306181373, 1370.220870732725871, 208.0282141261312461 ) ) ;
#94077=CARTESIAN_POINT ( 'NONE',  ( -8.698548410450724688, 1364.095994859965231, 207.6218459616988241 ) ) ;
#94085=CARTESIAN_POINT ( 'NONE',  ( -5.236338392959879684, 1368.774323667059889, 210.6218459616991936 ) ) ;
#94103=CARTESIAN_POINT ( 'NONE',  ( -8.337034337958552754, 1374.913060387289988, 204.5673033449591003 ) ) ;
#94118=CARTESIAN_POINT ( 'NONE',  ( -3.200208338885655479, 1370.366479271463049, 211.5769014320682970 ) ) ;
#94141=LINE ( 'NONE', #68983, #40060 ) ;
#94196=CARTESIAN_POINT ( 'NONE',  ( 3.148391675384991206, 1370.270822080606422, 210.8418201729652992 ) ) ;
#94226=CARTESIAN_POINT ( 'NONE',  ( -7.889195814119081440, 1372.293237941190000, 204.8119586455805177 ) ) ;
#94351=CARTESIAN_POINT ( 'NONE',  ( 10.02176186330000007, 1364.879735892739973, 207.6218459616989946 ) ) ;
#94366=CARTESIAN_POINT ( 'NONE',  ( 9.803099786913902491, 1368.651548183235036, 208.3718459617010978 ) ) ;
#94505=CARTESIAN_POINT ( 'NONE',  ( 1.895014057282678577, 1358.567760096916572, 208.3718459617010978 ) ) ;
#94564=VECTOR ( 'NONE', #107349, 1000.000000000000000 ) ;
#94634=CARTESIAN_POINT ( 'NONE',  ( -8.318057838368259738, 1363.950293616733916, 210.6218459617142003 ) ) ;
#94642=CARTESIAN_POINT ( 'NONE',  ( -7.052101012867634466, 1370.311329506408583, 209.6218459617033432 ) ) ;
#94848=DIRECTION ( 'NONE',  ( 6.123233995736769734E-17, 1.000000000000000000, 1.124819836996399911E-32 ) ) ;
#94928=CARTESIAN_POINT ( 'NONE',  ( 9.011028107012984734, 1364.896662482048669, 207.6218459616988241 ) ) ;
#94942=PRESENTATION_STYLE_ASSIGNMENT (( #35579 ) ) ;
#94944=CARTESIAN_POINT ( 'NONE',  ( 6.358435812139999754, 1368.427897723179740, 207.6218459616989946 ) ) ;
#94954=CARTESIAN_POINT ( 'NONE',  ( 7.877099145829999038, 1362.118768394180051, 207.6218459616989946 ) ) ;
#94968=CARTESIAN_POINT ( 'NONE',  ( -9.572080927779999334E-17, 1389.913060387289988, 209.1218459616989946 ) ) ;
#95008=AXIS2_PLACEMENT_3D ( 'NONE', #45620, #79760, #3067 ) ;
#95077=CARTESIAN_POINT ( 'NONE',  ( -2.581985620920249414, 1358.634824676206335, 208.3718459617010978 ) ) ;
#95101=CARTESIAN_POINT ( 'NONE',  ( -7.922050983617392461, 1365.299968594369147, 208.3718459617061285 ) ) ;
#95196=CARTESIAN_POINT ( 'NONE',  ( -7.744553022556359245, 1364.511030831803964, 209.6218459617148824 ) ) ;
#95204=CARTESIAN_POINT ( 'NONE',  ( -6.779714480667859533, 1369.556064268209411, 210.6218459617030021 ) ) ;
#95244=FILL_AREA_STYLE ('',( #79019 ) ) ;
#95428=CARTESIAN_POINT ( 'NONE',  ( -1.122592899216370017E-16, 1388.079727053959914, 209.1218459616989946 ) ) ;
#95463=ORIENTED_EDGE ( 'NONE', *, *, #109023, .T. ) ;
#95479=CARTESIAN_POINT ( 'NONE',  ( 9.971295257858800554, 1364.502667329735914, 210.6218459616987957 ) ) ;
#95492=CARTESIAN_POINT ( 'NONE',  ( 7.037448402365139799, 1370.316676987425353, 209.6218459617033432 ) ) ;
#95502=CARTESIAN_POINT ( 'NONE',  ( 0.05823133897989880153, 1360.390585217559874, 207.6218459616989946 ) ) ;
#95536=ORIENTED_EDGE ( 'NONE', *, *, #66449, .T. ) ;
#95592=ORIENTED_EDGE ( 'NONE', *, *, #106154, .F. ) ;
#95626=CARTESIAN_POINT ( 'NONE',  ( -4.171500989025269668, 1359.775974105520163, 207.6218459616987673 ) ) ;
#95652=CARTESIAN_POINT ( 'NONE',  ( -8.232155009531579637, 1367.485244382311976, 210.6218459616987957 ) ) ;
#95731=CARTESIAN_POINT ( 'NONE',  ( -2.929459774008567052, 1368.457002613392888, 210.4238567519766718 ) ) ;
#95746=CARTESIAN_POINT ( 'NONE',  ( -3.982247585419859792, 1360.759224656412016, 210.6218459616987957 ) ) ;
#95754=CARTESIAN_POINT ( 'NONE',  ( -8.696701630024261220, 1367.135748871425903, 210.6218459616991936 ) ) ;
#95832=CARTESIAN_POINT ( 'NONE',  ( 3.145310910306181373, 1370.220870732725871, 208.0282141261312461 ) ) ;
#95956=CARTESIAN_POINT ( 'NONE',  ( -3.061699073614430500, 1369.389631199361702, 207.6218459616989662 ) ) ;
#96027=CARTESIAN_POINT ( 'NONE',  ( 8.003402032965700741, 1365.192785687681635, 208.3718459617061285 ) ) ;
#96054=CARTESIAN_POINT ( 'NONE',  ( 9.663424421700000266, 1363.752474719049815, 207.6218459616989946 ) ) ;
#96180=CARTESIAN_POINT ( 'NONE',  ( 11.20850749315819428, 1362.682805967720014, 208.3718459617010978 ) ) ;
#96207=CARTESIAN_POINT ( 'NONE',  ( -6.899207507289689900, 1366.097715433741996, 208.3718459617061285 ) ) ;
#96263=CIRCLE ( 'NONE', #99838, 3.500000000000003109 ) ;
#96281=VERTEX_POINT ( 'NONE', #75764 ) ;
#96300=CARTESIAN_POINT ( 'NONE',  ( -3.755143501086812829, 1361.939125317512662, 210.6218459617142003 ) ) ;
#96308=CARTESIAN_POINT ( 'NONE',  ( -11.16448629964019190, 1365.517506221394797, 210.6218459617030021 ) ) ;
#96415=SPHERICAL_SURFACE ( 'NONE', #26535, 18.16666666670000296 ) ;
#96452=CARTESIAN_POINT ( 'NONE',  ( -9.977700672470000143, 1365.292605733889786, 210.6218459616991936 ) ) ;
#96511=CARTESIAN_POINT ( 'NONE',  ( -3.180365954810094209, 1370.226539215819685, 208.0370721656823321 ) ) ;
#96590=CARTESIAN_POINT ( 'NONE',  ( 8.106045534377265938, 1365.012046367625999, 208.3718459617061285 ) ) ;
#96616=CARTESIAN_POINT ( 'NONE',  ( -3.982247585420000124, 1360.759224656429978, 207.6218459616989946 ) ) ;
#96743=CARTESIAN_POINT ( 'NONE',  ( 10.63741388148666545, 1363.043374934216899, 210.6218459617030021 ) ) ;
#96768=CARTESIAN_POINT ( 'NONE',  ( -8.292274593569779029, 1366.175860171049408, 207.6218459616988241 ) ) ;
#96860=ORIENTED_EDGE ( 'NONE', *, *, #83626, .F. ) ;
#96869=CARTESIAN_POINT ( 'NONE',  ( -9.978586514379999883, 1364.539968386210148, 207.6218459616989946 ) ) ;
#96914=EDGE_LOOP ( 'NONE', ( #81168, #32823, #92690, #90837 ) ) ;
#97011=CARTESIAN_POINT ( 'NONE',  ( -6.376409808237344379, 1368.420764496007450, 210.6218459616991936 ) ) ;
#97041=ORIENTED_EDGE ( 'NONE', *, *, #92875, .F. ) ;
#97135=CARTESIAN_POINT ( 'NONE',  ( 8.653423937779999520, 1367.169888897630017, 207.6218459616989946 ) ) ;
#97150=CARTESIAN_POINT ( 'NONE',  ( 3.756023522784067925, 1369.098589419774044, 210.6218459616991936 ) ) ;
#97158=CARTESIAN_POINT ( 'NONE',  ( -9.505471540889999460, 1363.500209798499782, 207.6218459616989946 ) ) ;
#97276=CARTESIAN_POINT ( 'NONE',  ( 8.476942927299997876, 1362.523913559720086, 207.6218459616989946 ) ) ;
#97282=ORIENTED_EDGE ( 'NONE', *, *, #109023, .F. ) ;
#97301=CARTESIAN_POINT ( 'NONE',  ( -4.517103278725432602, 1368.953374755395998, 210.6218459616987957 ) ) ;
#97403=CARTESIAN_POINT ( 'NONE',  ( -12.04343452997959041, 1364.919544789908969, 209.6218459617033432 ) ) ;
#97489=AXIS2_PLACEMENT_3D ( 'NONE', #110379, #42630, #16292 ) ;
#97533=CIRCLE ( 'NONE', #54642, 17.27637083661241135 ) ;
#97580=VERTEX_POINT ( 'NONE', #94196 ) ;
#97680=CARTESIAN_POINT ( 'NONE',  ( 8.177749334224245104, 1366.009032010753117, 210.6218459617142003 ) ) ;
#97707=CARTESIAN_POINT ( 'NONE',  ( 9.369782510130001185, 1366.497526915280105, 207.6218459616989946 ) ) ;
#97731=B_SPLINE_CURVE_WITH_KNOTS ( 'NONE', 3,
 ( #109833, #110375, #41532, #85169, #51034, #40414, #74591, #94118 ),
 .UNSPECIFIED., .F., .F.,
 ( 4, 2, 2, 4 ),
 ( 0.0001376096082931063593, 0.003339882934058656990, 0.004941019596941432536, 0.006542156259824205913 ),
 .UNSPECIFIED. ) ;
#97820=CARTESIAN_POINT ( 'NONE',  ( 10.64129648661419658, 1361.926180408836444, 208.3718459617010978 ) ) ;
#97840=CARTESIAN_POINT ( 'NONE',  ( -9.978586514397619567, 1364.539968386201963, 210.6218459616987957 ) ) ;
#97941=CARTESIAN_POINT ( 'NONE',  ( -11.75150806997721276, 1363.816428733470957, 208.3718459617010978 ) ) ;
#97981=AXIS2_PLACEMENT_3D ( 'NONE', #22080, #32169, #90406 ) ;
#98023=CARTESIAN_POINT ( 'NONE',  ( 4.116054228253682723, 1370.396681933733362, 208.4739280433301758 ) ) ;
#98074=CARTESIAN_POINT ( 'NONE',  ( 3.005276066430000448, 1369.205039411269809, 210.6218459616989946 ) ) ;
#98087=CARTESIAN_POINT ( 'NONE',  ( -8.910387285859998840, 1362.858511851210096, 210.6218459616991936 ) ) ;
#98183=DIRECTION ( 'NONE',  ( -0.8775825618903726477, 1.203706215242023366E-32, -0.4794255386042032829 ) ) ;
#98224=CARTESIAN_POINT ( 'NONE',  ( 6.358435812117720687, 1368.427897723196111, 210.6218459616987957 ) ) ;
#98360=CARTESIAN_POINT ( 'NONE',  ( 3.854212611492175977, 1362.772174771310119, 209.6218459617148824 ) ) ;
#98376=CARTESIAN_POINT ( 'NONE',  ( 9.432497968925920517, 1361.986403221846331, 207.6218459616987673 ) ) ;
#98398=CARTESIAN_POINT ( 'NONE',  ( -8.791275945972083505, 1364.761074005578166, 210.6218459617142003 ) ) ;
#98420=CARTESIAN_POINT ( 'NONE',  ( -2.887264227133756744, 1368.159418877311282, 210.2902280133655211 ) ) ;
#98498=CARTESIAN_POINT ( 'NONE',  ( -11.32094776019573956, 1366.953380474498545, 208.3718459617010978 ) ) ;
#98551=CARTESIAN_POINT ( 'NONE',  ( -3.061616997868380553E-17, 1389.413060387289988, 209.1218459616989946 ) ) ;
#98602=VERTEX_POINT ( 'NONE', #29237 ) ;
#98623=CARTESIAN_POINT ( 'NONE',  ( 3.149414619133680482, 1370.221588481574372, 210.2153961732977905 ) ) ;
#98636=CARTESIAN_POINT ( 'NONE',  ( 9.622136349630000751, 1363.684386430209997, 210.6218459616991936 ) ) ;
#98776=CARTESIAN_POINT ( 'NONE',  ( 4.283227215352179762, 1367.979132611802015, 207.6218459616988241 ) ) ;
#98906=CARTESIAN_POINT ( 'NONE',  ( 3.426613460960548085, 1360.656565846677722, 210.6218459616987957 ) ) ;
#98923=CARTESIAN_POINT ( 'NONE',  ( 11.45468757771786450, 1366.970939356060853, 209.6218459617033432 ) ) ;
#98943=CARTESIAN_POINT ( 'NONE',  ( -8.790915045283584917, 1365.067705246386822, 210.6218459617142003 ) ) ;
#99039=CARTESIAN_POINT ( 'NONE',  ( -10.68489437346363857, 1363.121218440984649, 210.6218459617030021 ) ) ;
#99063=CARTESIAN_POINT ( 'NONE',  ( -3.180365954794715400, 1370.226539215816501, 210.2066197577219100 ) ) ;
#99141=CARTESIAN_POINT ( 'NONE',  ( -2.919110404717550011, 1368.384062535930070, 207.8228080779019820 ) ) ;
#99312=CARTESIAN_POINT ( 'NONE',  ( 7.975220293214148271, 1366.176009064089612, 210.6218459617142003 ) ) ;
#99338=CARTESIAN_POINT ( 'NONE',  ( 6.358435812139999754, 1368.427897723179740, 207.6218459616989946 ) ) ;
#99381=CARTESIAN_POINT ( 'NONE',  ( -4.366757940789628201, 1370.449312398489383, 209.4870077725456667 ) ) ;
#99405=DIRECTION ( 'NONE',  ( 3.828568698926946970E-16, 0.000000000000000000, -1.000000000000000000 ) ) ;
#99447=CARTESIAN_POINT ( 'NONE',  ( 1.592937850129041877, 1362.438491279120626, 209.6218459617148824 ) ) ;
#99463=CARTESIAN_POINT ( 'NONE',  ( 10.34804584725118737, 1366.870369466032798, 207.6218459616987673 ) ) ;
#99483=CARTESIAN_POINT ( 'NONE',  ( -7.988512957371035839, 1364.858218297605163, 209.6218459617148824 ) ) ;
#99503=DIRECTION ( 'NONE',  ( -6.123233995736769734E-17, -1.000000000000000000, -1.124819836996399911E-32 ) ) ;
#99589=CARTESIAN_POINT ( 'NONE',  ( -9.692061980449199865, 1363.802329763672105, 210.6218459616991936 ) ) ;
#99725=CARTESIAN_POINT ( 'NONE',  ( -3.268503196014072465, 1371.061470524529796, 208.3718459617010978 ) ) ;
#99728=CARTESIAN_POINT ( 'NONE',  ( 1.748848150599999984, 1360.440694539930064, 210.6218459616991936 ) ) ;
#99838=AXIS2_PLACEMENT_3D ( 'NONE', #46223, #106103, #89844 ) ;
#99850=ORIENTED_EDGE ( 'NONE', *, *, #102365, .F. ) ;
#99919=STYLED_ITEM ( 'NONE', ( #52705 ), #84353 ) ;
#100005=CARTESIAN_POINT ( 'NONE',  ( 7.699968550499718845, 1364.464658747520616, 209.6218459617148824 ) ) ;
#100021=CARTESIAN_POINT ( 'NONE',  ( 11.10947396198625370, 1365.784518360480661, 210.6218459617030021 ) ) ;
#100158=CARTESIAN_POINT ( 'NONE',  ( -11.37099373375535727, 1362.708999033907048, 209.6218459617033432 ) ) ;
#100230=DIRECTION ( 'NONE',  ( 3.828568698926946970E-16, 0.000000000000000000, -1.000000000000000000 ) ) ;
#100231=LINE ( 'NONE', #15635, #101727 ) ;
#100331=CARTESIAN_POINT ( 'NONE',  ( 8.775825618903720482, 1379.913060387289988, 213.9161013477410336 ) ) ;
#100558=CARTESIAN_POINT ( 'NONE',  ( 8.606858817780835835, 1364.325397926196729, 210.6218459617142003 ) ) ;
#100573=CARTESIAN_POINT ( 'NONE',  ( 9.943976501836180759, 1365.461622992593902, 210.6218459616991936 ) ) ;
#100696=CARTESIAN_POINT ( 'NONE',  ( -10.23589100247646577, 1362.489324292358333, 210.6218459617030021 ) ) ;
#100749=ADVANCED_FACE ( 'NONE', ( #34839 ), #96415, .T. ) ;
#100940=AXIS2_PLACEMENT_3D ( 'NONE', #87881, #13326, #80566 ) ;
#100964=CARTESIAN_POINT ( 'NONE',  ( -0.01912654351157340102, 1347.931987472819856, 209.1220808601199792 ) ) ;
#101035=CARTESIAN_POINT ( 'NONE',  ( -3.737177908446197794, 1370.322789966642176, 210.0021808679227888 ) ) ;
#101096=CARTESIAN_POINT ( 'NONE',  ( 7.383230514405129341, 1364.047475561790179, 208.3718459617061285 ) ) ;
#101099=EDGE_LOOP ( 'NONE', ( #24344, #23584 ) ) ;
#101113=CARTESIAN_POINT ( 'NONE',  ( 11.64244948864622664, 1363.185827771890899, 209.6218459617033432 ) ) ;
#101233=CARTESIAN_POINT ( 'NONE',  ( -9.251045835782019111, 1361.603097335492066, 210.6218459617030021 ) ) ;
#101372=VERTEX_POINT ( 'NONE', #43962 ) ;
#101582=CARTESIAN_POINT ( 'NONE',  ( -3.324921645876977472, 1370.249766618262356, 208.0786078478728314 ) ) ;
#101583=DIRECTION ( 'NONE',  ( -0.8775825618903720926, 0.000000000000000000, -0.4794255386042041156 ) ) ;
#101641=AXIS2_PLACEMENT_3D ( 'NONE', #41932, #82817, #102375 ) ;
#101642=CARTESIAN_POINT ( 'NONE',  ( 6.890671329650879251, 1363.865351280181812, 209.6218459617148824 ) ) ;
#101655=( NAMED_UNIT ( * ) SI_UNIT ( $, .STERADIAN. ) SOLID_ANGLE_UNIT ( ) );
#101658=CARTESIAN_POINT ( 'NONE',  ( 7.818221670759999853, 1367.736483592530021, 207.6218459616989946 ) ) ;
#101727=VECTOR ( 'NONE', #17287, 1000.000000000000114 ) ;
#101796=CARTESIAN_POINT ( 'NONE',  ( 0.05823133897708447637, 1360.390585217553962, 210.6218459616991936 ) ) ;
#101917=CARTESIAN_POINT ( 'NONE',  ( -7.951048262496951402, 1364.788525692098119, 209.6218459617148824 ) ) ;
#101919=AXIS2_PLACEMENT_3D ( 'NONE', #30184, #54874, #64376 ) ;
#102211=CARTESIAN_POINT ( 'NONE',  ( 7.383885237739054475, 1362.992059837184343, 207.6218459616988241 ) ) ;
#102227=CARTESIAN_POINT ( 'NONE',  ( 9.879744843524427722, 1368.750325468937035, 209.6218459617033432 ) ) ;
#102358=CARTESIAN_POINT ( 'NONE',  ( 6.135919523401898168, 1359.334529397649248, 208.3718459617010978 ) ) ;
#102362=ORIENTED_EDGE ( 'NONE', *, *, #73258, .F. ) ;
#102365=EDGE_CURVE ( 'NONE', #25781, #39065, #71355, .T. ) ;
#102375=DIRECTION ( 'NONE',  ( 3.828568698926946970E-16, 0.000000000000000000, -1.000000000000000000 ) ) ;
#102473=CARTESIAN_POINT ( 'NONE',  ( -8.119505269034053896, 1363.763538997089199, 210.6218459617142003 ) ) ;
#102482=CARTESIAN_POINT ( 'NONE',  ( -9.766226206179759117, 1367.813519127536438, 210.6218459617030021 ) ) ;
#102602=CARTESIAN_POINT ( 'NONE',  ( -2.919081270098979441, 1368.383855509380055, 210.4211783971049954 ) ) ;
#102708=ORIENTED_EDGE ( 'NONE', *, *, #110303, .F. ) ;
#102744=CARTESIAN_POINT ( 'NONE',  ( 8.899640782778483583, 1364.433807194531028, 207.6218459616988241 ) ) ;
#102758=CARTESIAN_POINT ( 'NONE',  ( 9.961564800042728152, 1367.346295917899852, 207.6218459616987673 ) ) ;
#102826=ORIENTED_EDGE ( 'NONE', *, *, #48439, .T. ) ;
#102828=EDGE_CURVE ( 'NONE', #76110, #101372, #56584, .T. ) ;
#102898=CARTESIAN_POINT ( 'NONE',  ( 1.842394330875738673, 1359.242016496408041, 210.6218459617030021 ) ) ;
#102923=CARTESIAN_POINT ( 'NONE',  ( -3.406640539343045671, 1367.128124208074041, 209.6218459617148824 ) ) ;
#103022=CARTESIAN_POINT ( 'NONE',  ( -8.461434042299536884, 1363.810109312981240, 207.6218459616988241 ) ) ;
#103030=CARTESIAN_POINT ( 'NONE',  ( -8.962252599297759303, 1366.920250605815909, 210.6218459616991936 ) ) ;
#103087=DIRECTION ( 'NONE',  ( -0.4794255386042020062, 2.935634756405659852E-17, 0.8775825618903733139 ) ) ;
#103170=DIRECTION ( 'NONE',  ( 3.828568698926945491E-16, 0.000000000000000000, -1.000000000000000000 ) ) ;
#103298=CARTESIAN_POINT ( 'NONE',  ( 9.842969107833919651, 1365.740588703670028, 210.6218459616987957 ) ) ;
#103315=CARTESIAN_POINT ( 'NONE',  ( 9.478478336866400511, 1368.047529015550481, 210.6218459617030021 ) ) ;
#103326=CARTESIAN_POINT ( 'NONE',  ( -8.962252599310001955, 1366.920250605820002, 207.6218459616989946 ) ) ;
#103455=CARTESIAN_POINT ( 'NONE',  ( 3.426613460956668078, 1360.656565846701824, 210.6218459616991936 ) ) ;
#103483=CARTESIAN_POINT ( 'NONE',  ( -8.484789816894487302, 1365.990492769855791, 207.6218459616988241 ) ) ;
#103519=COLOUR_RGB ( '', 0.40784314, 0.44705882, 0.49803922) ;
#103591=CARTESIAN_POINT ( 'NONE',  ( -6.341401618134332452, 1363.580025761456227, 209.6218459617148824 ) ) ;
#103600=CARTESIAN_POINT ( 'NONE',  ( -5.236338392940000475, 1368.774323667059889, 207.6218459616989946 ) ) ;
#103656=CARTESIAN_POINT ( 'NONE',  ( -2.813821217502529670, 1367.641464860501173, 208.8602496609475168 ) ) ;
#103729=AXIS2_PLACEMENT_3D ( 'NONE', #41112, #51176, #15341 ) ;
#103758=ORIENTED_EDGE ( 'NONE', *, *, #43488, .T. ) ;
#103817=AXIS2_PLACEMENT_3D ( 'NONE', #89295, #12591, #4197 ) ;
#103875=CARTESIAN_POINT ( 'NONE',  ( 8.122847524725520074, 1364.881652834217903, 208.3718459617061285 ) ) ;
#103891=CARTESIAN_POINT ( 'NONE',  ( 7.818221670731199779, 1367.736483592526156, 210.6218459616991936 ) ) ;
#103901=CARTESIAN_POINT ( 'NONE',  ( 6.892224678239999847, 1361.632554499750086, 207.6218459616989946 ) ) ;
#103904=( GEOMETRIC_REPRESENTATION_CONTEXT ( 3 ) GLOBAL_UNCERTAINTY_ASSIGNED_CONTEXT ( ( #59222 ) ) GLOBAL_UNIT_ASSIGNED_CONTEXT ( ( #43444, #78130, #68112 ) ) REPRESENTATION_CONTEXT ( 'NONE', 'WORKASPACE' ) );
#103953=DIRECTION ( 'NONE',  ( -6.123233995736769734E-17, -1.000000000000000000, 7.888609052210119587E-33 ) ) ;
#104020=CARTESIAN_POINT ( 'NONE',  ( -5.209651373121763740, 1358.975734498126940, 209.6218459617033432 ) ) ;
#104046=CARTESIAN_POINT ( 'NONE',  ( -8.016541010710112047, 1366.397902625823463, 207.6218459616988241 ) ) ;
#104085=EDGE_CURVE ( 'NONE', #32037, #52548, #78502, .T. ) ;
#104145=CARTESIAN_POINT ( 'NONE',  ( 6.424778925410263852, 1362.739727695628744, 210.6218459617142003 ) ) ;
#104153=CARTESIAN_POINT ( 'NONE',  ( -8.624710350811819026, 1367.191948709361895, 210.6218459616991936 ) ) ;
#104366=EDGE_CURVE ( 'NONE', #36878, #15971, #100231, .T. ) ;
#104430=CARTESIAN_POINT ( 'NONE',  ( 9.532517564039318714, 1366.286862064878051, 210.6218459616987957 ) ) ;
#104453=CARTESIAN_POINT ( 'NONE',  ( -7.173827098650000345, 1361.757975858899954, 207.6218459616989946 ) ) ;
#104492=EDGE_CURVE ( 'NONE', #74455, #96281, #28459, .T. ) ;
#104579=CARTESIAN_POINT ( 'NONE',  ( 10.93866963977056983, 1362.275162845329533, 208.3718459617010978 ) ) ;
#104605=CARTESIAN_POINT ( 'NONE',  ( -4.973616640903610886, 1367.807959820899441, 207.6218459616988241 ) ) ;
#104680=CARTESIAN_POINT ( 'NONE',  ( -2.979756015838803229, 1368.811721020882487, 207.6609286928419067 ) ) ;
#104694=CARTESIAN_POINT ( 'NONE',  ( -5.613600279743296895, 1362.409757668945758, 210.6218459617142003 ) ) ;
#104702=CARTESIAN_POINT ( 'NONE',  ( -7.984337885465997431, 1369.008371754427117, 210.6218459617030021 ) ) ;
#104757=CARTESIAN_POINT ( 'NONE',  ( -2.919110404717550011, 1368.384062535930070, 207.8228080779019820 ) ) ;
#104758=EDGE_CURVE ( 'NONE', #25781, #52548, #53022, .T. ) ;
#104776=DIRECTION ( 'NONE',  ( 0.8539859765994181062, 0.000000000000000000, -0.5202960232132650686 ) ) ;
#104849=CARTESIAN_POINT ( 'NONE',  ( -9.978586514389998996, 1364.539968386210148, 210.6218459616991936 ) ) ;
#104911=CARTESIAN_POINT ( 'NONE',  ( -3.138099469817183351, 1369.928451332881878, 207.8004044997916537 ) ) ;
#104984=CARTESIAN_POINT ( 'NONE',  ( 10.02176186329304031, 1364.879735892739745, 210.6218459616987957 ) ) ;
#105000=CARTESIAN_POINT ( 'NONE',  ( 3.173741429363529321, 1370.393155323753945, 210.6218459617030021 ) ) ;
#105012=CARTESIAN_POINT ( 'NONE',  ( 5.604365146370000161, 1361.139420828410039, 207.6218459616989946 ) ) ;
#105082=CIRCLE ( 'NONE', #106824, 9.500000000000008882 ) ;
#105103=ORIENTED_EDGE ( 'NONE', *, *, #108310, .F. ) ;
#105136=CARTESIAN_POINT ( 'NONE',  ( 7.671300932945157136, 1359.787265839942847, 209.6218459617033432 ) ) ;
#105160=CARTESIAN_POINT ( 'NONE',  ( -8.962252599314020074, 1366.920250605834099, 210.6218459616987957 ) ) ;
#105258=CARTESIAN_POINT ( 'NONE',  ( -9.832966357650001044, 1364.062280235949856, 207.6218459616989946 ) ) ;
#105317=DIRECTION ( 'NONE',  ( -0.8775825618903726477, 1.203706215242023366E-32, -0.4794255386042032829 ) ) ;
#105404=CARTESIAN_POINT ( 'NONE',  ( -8.232155009530000456, 1367.485244382299925, 210.6218459616991936 ) ) ;
#105467=CONICAL_SURFACE ( 'NONE', #55422, 23.60273273060006360, 1.047194910839999826 ) ;
#105546=CARTESIAN_POINT ( 'NONE',  ( 7.445922712514740915, 1367.935115748543922, 210.6218459616987957 ) ) ;
#105573=CARTESIAN_POINT ( 'NONE',  ( -9.328535443860001664, 1363.278783432130012, 207.6218459616989946 ) ) ;
#105702=CARTESIAN_POINT ( 'NONE',  ( 9.060256214184169821, 1361.711347158616718, 207.6218459616987673 ) ) ;
#105725=CARTESIAN_POINT ( 'NONE',  ( -5.962554884090152996, 1367.290268553626447, 210.6218459617142003 ) ) ;
#105741=DIRECTION ( 'NONE',  ( 3.828568698926946970E-16, 0.000000000000000000, -1.000000000000000000 ) ) ;
#105803=CARTESIAN_POINT ( 'NONE',  ( 3.138931148605959913E-16, 1391.413060387289988, 209.1218459616989946 ) ) ;
#105804=CARTESIAN_POINT ( 'NONE',  ( -3.034926079678203159, 1369.200812461396481, 210.6218459616991936 ) ) ;
#105825=CARTESIAN_POINT ( 'NONE',  ( -10.75152334329300174, 1366.170224226380697, 207.6218459616987673 ) ) ;
#105965=CARTESIAN_POINT ( 'NONE',  ( -9.936738324549999390, 1364.340818343089950, 210.6218459616991936 ) ) ;
#106086=CARTESIAN_POINT ( 'NONE',  ( 7.770954596407177561, 1365.285754389724843, 209.6218459617148824 ) ) ;
#106102=CARTESIAN_POINT ( 'NONE',  ( 3.005276066430516035, 1369.205039411270036, 210.6218459616991936 ) ) ;
#106103=DIRECTION ( 'NONE',  ( 6.123233995736769734E-17, 1.000000000000000000, 1.124819836996399911E-32 ) ) ;
#106154=EDGE_CURVE ( 'NONE', #74686, #33810, #83152, .T. ) ;
#106233=CARTESIAN_POINT ( 'NONE',  ( 8.863526962015209065, 1360.372185508180110, 209.6218459617033432 ) ) ;
#106257=CARTESIAN_POINT ( 'NONE',  ( -8.121924544136929214, 1364.961891190665483, 208.3718459617061285 ) ) ;
#106356=CARTESIAN_POINT ( 'NONE',  ( -9.657355732011760452, 1366.083296228048084, 210.6218459616991936 ) ) ;
#106426=FACE_OUTER_BOUND ( 'NONE', #109807, .T. ) ;
#106499=CARTESIAN_POINT ( 'NONE',  ( -0.7618909056620021270, 1360.403425203259985, 210.6218459616991936 ) ) ;
#106624=CARTESIAN_POINT ( 'NONE',  ( 7.230203487789204964, 1365.895265398900847, 208.3718459617061285 ) ) ;
#106649=CARTESIAN_POINT ( 'NONE',  ( 5.215187551879999717, 1368.779556716650177, 207.6218459616989946 ) ) ;
#106756=CARTESIAN_POINT ( 'NONE',  ( 0.05319939914973582928, 1362.392533002544042, 209.6218459617148824 ) ) ;
#106771=CARTESIAN_POINT ( 'NONE',  ( 9.930155807529674306, 1362.158223026690166, 210.6218459617030021 ) ) ;
#106794=CARTESIAN_POINT ( 'NONE',  ( -9.351945459739999578, 1366.519103298159735, 207.6218459616989946 ) ) ;
#106824=AXIS2_PLACEMENT_3D ( 'NONE', #85480, #42960, #86603 ) ;
#106877=DIRECTION ( 'NONE',  ( -0.8775825618903725367, 0.000000000000000000, -0.4794255386042032829 ) ) ;
#106896=CARTESIAN_POINT ( 'NONE',  ( -9.516636888329999877, 1366.309137899869938, 207.6218459616989946 ) ) ;
#106897=PLANE ( 'NONE',  #101919 ) ;
#106937=AXIS2_PLACEMENT_3D ( 'NONE', #19154, #79114, #88613 ) ;
#107046=CARTESIAN_POINT ( 'NONE',  ( 7.445922712500000706, 1367.935115748530052, 210.6218459616991936 ) ) ;
#107059=DIRECTION ( 'NONE',  ( -6.123233995736769734E-17, -1.000000000000000000, 0.000000000000000000 ) ) ;
#107181=CARTESIAN_POINT ( 'NONE',  ( 4.064762469398819356, 1367.001946128230202, 209.6218459617148824 ) ) ;
#107315=CARTESIAN_POINT ( 'NONE',  ( 0.05521217508070846297, 1361.591753888529865, 210.6218459617142003 ) ) ;
#107331=CARTESIAN_POINT ( 'NONE',  ( 9.971295257839999593, 1364.502667329740007, 207.6218459616989946 ) ) ;
#107335=CARTESIAN_POINT ( 'NONE',  ( -3.034926079678203159, 1369.200812461396481, 210.6218459616991936 ) ) ;
#107337=ORIENTED_EDGE ( 'NONE', *, *, #18113, .T. ) ;
#107349=DIRECTION ( 'NONE',  ( -0.6038592750913978069, -0.7071067811868650965, 0.3679048462383208151 ) ) ;
#107354=CARTESIAN_POINT ( 'NONE',  ( -8.775285687485823161, 1364.676427693243795, 210.6218459617142003 ) ) ;
#107392=CIRCLE ( 'NONE', #87762, 3.000000000000002665 ) ;
#107449=CARTESIAN_POINT ( 'NONE',  ( -10.96668869512642708, 1365.480022806811803, 207.6218459616987673 ) ) ;
#107478=ORIENTED_EDGE ( 'NONE', *, *, #69028, .T. ) ;
#107561=CARTESIAN_POINT ( 'NONE',  ( 2.880867337579580134, 1368.384084939549894, 207.8228488383560091 ) ) ;
#107588=CARTESIAN_POINT ( 'NONE',  ( 5.805282093358999695, 1389.008761609309886, 209.1218459616989946 ) ) ;
#107595=CARTESIAN_POINT ( 'NONE',  ( 8.476942927309998765, 1362.523913559719858, 210.6218459616991936 ) ) ;
#107669=B_SPLINE_CURVE_WITH_KNOTS ( 'NONE', 3,
 ( #89732, #55608, #38770, #56691, #72944, #90827 ),
 .UNSPECIFIED., .F., .F.,
 ( 4, 2, 4 ),
 ( 0.003574833876271631995, 0.004151067118842836218, 0.004727300361414039573 ),
 .UNSPECIFIED. ) ;
#107734=CARTESIAN_POINT ( 'NONE',  ( 7.474134278654832819, 1365.552169080253861, 209.6218459617148824 ) ) ;
#107761=CARTESIAN_POINT ( 'NONE',  ( 7.445922712490000706, 1367.935115748530052, 207.6218459616989946 ) ) ;
#107843=ORIENTED_EDGE ( 'NONE', *, *, #57628, .F. ) ;
#107861=CARTESIAN_POINT ( 'NONE',  ( -2.179640835936603960, 1362.370409203572308, 208.3718459617061285 ) ) ;
#107877=CARTESIAN_POINT ( 'NONE',  ( 11.84442987637726930, 1365.578918197742496, 208.3718459617010978 ) ) ;
#107900=CARTESIAN_POINT ( 'NONE',  ( -9.978586514379999883, 1364.539968386210148, 207.6218459616989946 ) ) ;
#107999=CARTESIAN_POINT ( 'NONE',  ( -9.178315062057500029, 1363.109187794154195, 210.6218459616991936 ) ) ;
#108138=FACE_OUTER_BOUND ( 'NONE', #48192, .T. ) ;
#108310=EDGE_CURVE ( 'NONE', #63480, #92455, #44700, .T. ) ;
#108418=CARTESIAN_POINT ( 'NONE',  ( 7.930007129861151860, 1364.752738923533116, 209.6218459617148824 ) ) ;
#108422=ORIENTED_EDGE ( 'NONE', *, *, #63923, .T. ) ;
#108436=CARTESIAN_POINT ( 'NONE',  ( 10.76932834697634611, 1366.129144616212216, 207.6218459616987673 ) ) ;
#108460=CARTESIAN_POINT ( 'NONE',  ( -8.910739657505105882, 1364.460249266779101, 207.6218459616988241 ) ) ;
#108481=ORIENTED_EDGE ( 'NONE', *, *, #41059, .F. ) ;
#108559=CARTESIAN_POINT ( 'NONE',  ( -10.74627850421423680, 1362.045253526237047, 208.3718459617010978 ) ) ;
#108694=CARTESIAN_POINT ( 'NONE',  ( -3.005276066430000448, 1369.205039411269809, 207.6218459616989946 ) ) ;
#108697=CARTESIAN_POINT ( 'NONE',  ( 5.604365146380000162, 1361.139420828400034, 210.6218459616991936 ) ) ;
#108753=CARTESIAN_POINT ( 'NONE',  ( -2.561957929796738309, 1389.413060387289988, 210.6827340313378443 ) ) ;
#108908=DIRECTION ( 'NONE',  ( 0.4794255386042041156, -5.511896626706601104E-17, -0.8775825618903722036 ) ) ;
#108976=CARTESIAN_POINT ( 'NONE',  ( 7.602738516744689257, 1364.209988717608212, 208.3718459617061285 ) ) ;
#108994=CARTESIAN_POINT ( 'NONE',  ( 11.76506628332722748, 1365.966147004922504, 208.3718459617010978 ) ) ;
#109023=EDGE_CURVE ( 'NONE', #63480, #66318, #97731, .T. ) ;
#109070=CIRCLE ( 'NONE', #26809, 8.989690721650012151 ) ;
#109088=CARTESIAN_POINT ( 'NONE',  ( -3.034926079678273325, 1369.200812461397618, 207.6218459616989946 ) ) ;
#109130=CARTESIAN_POINT ( 'NONE',  ( -9.132344861692528681, 1361.764119804333177, 207.6218459616987673 ) ) ;
#109191=CARTESIAN_POINT ( 'NONE',  ( 3.005276066430000448, 1369.205039411269809, 207.6218459616989946 ) ) ;
#109400=DIRECTION ( 'NONE',  ( -1.000000000000000000, 0.000000000000000000, -1.254859372443971704E-14 ) ) ;
#109468=FACE_OUTER_BOUND ( 'NONE', #89964, .T. ) ;
#109525=CARTESIAN_POINT ( 'NONE',  ( 7.285242456129513045, 1363.166718125769876, 210.6218459617142003 ) ) ;
#109544=CARTESIAN_POINT ( 'NONE',  ( 11.03249561956813274, 1364.862809303433096, 207.6218459616987673 ) ) ;
#109610=CARTESIAN_POINT ( 'NONE',  ( -0.01912654351157340102, 1347.931987472819856, 209.1220808601199792 ) ) ;
#109669=CARTESIAN_POINT ( 'NONE',  ( -11.01845241045810120, 1362.383112808261785, 208.3718459617010978 ) ) ;
#109804=EDGE_CURVE ( 'NONE', #3293, #5019, #57489, .T. ) ;
#109807=EDGE_LOOP ( 'NONE', ( #96860, #62357, #48535, #42767, #64969 ) ) ;
#109833=CARTESIAN_POINT ( 'NONE',  ( 3.160865718646527434, 1370.358796302880364, 211.5724212009420739 ) ) ;
#109952=ORIENTED_EDGE ( 'NONE', *, *, #7636, .T. ) ;
#109966=CIRCLE ( 'NONE', #97489, 1.500287545630077490 ) ;
#110011=SPHERICAL_SURFACE ( 'NONE', #87996, 18.16666666670000296 ) ;
#110070=CARTESIAN_POINT ( 'NONE',  ( 6.502686550879601235, 1362.555198829660185, 207.6218459616988241 ) ) ;
#110085=CARTESIAN_POINT ( 'NONE',  ( 0.000000000000000000, 0.000000000000000000, 0.000000000000000000 ) ) ;
#110087=CARTESIAN_POINT ( 'NONE',  ( 6.765843366259869818, 1369.561165281723333, 210.6218459617030021 ) ) ;
#110213=CARTESIAN_POINT ( 'NONE',  ( -7.590039838923934745, 1360.846950907609425, 207.6218459616987673 ) ) ;
#110303=EDGE_CURVE ( 'NONE', #74686, #88920, #79476, .T. ) ;
#110337=CARTESIAN_POINT ( 'NONE',  ( -7.351830250119061105, 1364.179456836979853, 209.6218459617148824 ) ) ;
#110375=CARTESIAN_POINT ( 'NONE',  ( 2.122041310277463566, 1370.144953969707558, 211.3659795828131109 ) ) ;
#110379=CARTESIAN_POINT ( 'NONE',  ( 2.986193535308999891, 1369.126893976419979, 209.1220808601199792 ) ) ;
#110492=CARTESIAN_POINT ( 'NONE',  ( 3.756023522790000069, 1369.098589419769951, 207.6218459616989946 ) ) ;
#110621=CARTESIAN_POINT ( 'NONE',  ( 6.907476780246043724, 1362.740070248910570, 207.6218459616988241 ) ) ;
#110634=CARTESIAN_POINT ( 'NONE',  ( 4.501691961449999724, 1368.956319095359959, 207.6218459616989946 ) ) ;
#110641=ORIENTED_EDGE ( 'NONE', *, *, #72662, .T. ) ;
#110697=CIRCLE ( 'NONE', #85675, 3.000000000000002665 ) ;
#110768=CARTESIAN_POINT ( 'NONE',  ( 4.262353028403936150, 1360.811275533940034, 210.6218459616991936 ) ) ;
#110796=AXIS2_PLACEMENT_3D ( 'NONE', #82386, #56638, #29228 ) ;
#110798=ADVANCED_BREP_SHAPE_REPRESENTATION ( '', ( #84353, #21632 ), #103904 ) ;
ENDSEC;
END-ISO-10303-21;
